ISO-10303-21;
HEADER;
/* Generated by software containing ST-Developer
 * from STEP Tools, Inc. (www.steptools.com) 
 */

FILE_DESCRIPTION(
/* description */ ('PAT-122'),
/* implementation_level */ '2;1');

FILE_NAME(
/* name */ '360 mm cross member.step',
/* time_stamp */ '2026-10-29T20:20:12-07:00',
/* author */ (''),
/* organization */ (''),
/* preprocessor_version */ 'ST-DEVELOPER v20.2',
/* originating_system */ 'Autodesk Translation Framework v15.17.0.0',
/* authorisation */ '');

FILE_SCHEMA (('AUTOMOTIVE_DESIGN { 1 0 10303 214 3 1 1 }'));
ENDSEC;

DATA;
#10=MECHANICAL_DESIGN_GEOMETRIC_PRESENTATION_REPRESENTATION('',(#505),#10019);
#461=SHAPE_REPRESENTATION_RELATIONSHIP('SRR','None',#10182,#483);
#483=ADVANCED_BREP_SHAPE_REPRESENTATION('',(#527),#10011);
#505=STYLED_ITEM('',(#10362),#527);
#527=MANIFOLD_SOLID_BREP('Body1',#5627);
#597=FACE_BOUND('',#1337,.T.);
#598=FACE_BOUND('',#1384,.T.);
#717=PLANE('',#6133);
#718=PLANE('',#6135);
#719=PLANE('',#6136);
#720=PLANE('',#6137);
#721=PLANE('',#6138);
#722=PLANE('',#6139);
#723=PLANE('',#6140);
#724=PLANE('',#6141);
#725=PLANE('',#6142);
#726=PLANE('',#6143);
#727=PLANE('',#6144);
#728=PLANE('',#6145);
#729=PLANE('',#6146);
#730=PLANE('',#6147);
#731=PLANE('',#6148);
#732=PLANE('',#6149);
#733=PLANE('',#6150);
#734=PLANE('',#6151);
#735=PLANE('',#6152);
#736=PLANE('',#6153);
#737=PLANE('',#6154);
#738=PLANE('',#6155);
#739=PLANE('',#6156);
#740=PLANE('',#6157);
#741=PLANE('',#6158);
#742=PLANE('',#6159);
#743=PLANE('',#6160);
#744=PLANE('',#6161);
#745=PLANE('',#6162);
#746=PLANE('',#6163);
#747=PLANE('',#6164);
#748=PLANE('',#6165);
#749=PLANE('',#6166);
#750=PLANE('',#6167);
#751=PLANE('',#6168);
#752=PLANE('',#6169);
#753=PLANE('',#6170);
#754=PLANE('',#6171);
#755=PLANE('',#6172);
#756=PLANE('',#6173);
#757=PLANE('',#6174);
#758=PLANE('',#6177);
#759=PLANE('',#6178);
#760=PLANE('',#6179);
#761=PLANE('',#6180);
#762=PLANE('',#6181);
#978=FACE_OUTER_BOUND('',#1336,.T.);
#979=FACE_OUTER_BOUND('',#1338,.T.);
#980=FACE_OUTER_BOUND('',#1339,.T.);
#981=FACE_OUTER_BOUND('',#1340,.T.);
#982=FACE_OUTER_BOUND('',#1341,.T.);
#983=FACE_OUTER_BOUND('',#1342,.T.);
#984=FACE_OUTER_BOUND('',#1343,.T.);
#985=FACE_OUTER_BOUND('',#1344,.T.);
#986=FACE_OUTER_BOUND('',#1345,.T.);
#987=FACE_OUTER_BOUND('',#1346,.T.);
#988=FACE_OUTER_BOUND('',#1347,.T.);
#989=FACE_OUTER_BOUND('',#1348,.T.);
#990=FACE_OUTER_BOUND('',#1349,.T.);
#991=FACE_OUTER_BOUND('',#1350,.T.);
#992=FACE_OUTER_BOUND('',#1351,.T.);
#993=FACE_OUTER_BOUND('',#1352,.T.);
#994=FACE_OUTER_BOUND('',#1353,.T.);
#995=FACE_OUTER_BOUND('',#1354,.T.);
#996=FACE_OUTER_BOUND('',#1355,.T.);
#997=FACE_OUTER_BOUND('',#1356,.T.);
#998=FACE_OUTER_BOUND('',#1357,.T.);
#999=FACE_OUTER_BOUND('',#1358,.T.);
#1000=FACE_OUTER_BOUND('',#1359,.T.);
#1001=FACE_OUTER_BOUND('',#1360,.T.);
#1002=FACE_OUTER_BOUND('',#1361,.T.);
#1003=FACE_OUTER_BOUND('',#1362,.T.);
#1004=FACE_OUTER_BOUND('',#1363,.T.);
#1005=FACE_OUTER_BOUND('',#1364,.T.);
#1006=FACE_OUTER_BOUND('',#1365,.T.);
#1007=FACE_OUTER_BOUND('',#1366,.T.);
#1008=FACE_OUTER_BOUND('',#1367,.T.);
#1009=FACE_OUTER_BOUND('',#1368,.T.);
#1010=FACE_OUTER_BOUND('',#1369,.T.);
#1011=FACE_OUTER_BOUND('',#1370,.T.);
#1012=FACE_OUTER_BOUND('',#1371,.T.);
#1013=FACE_OUTER_BOUND('',#1372,.T.);
#1014=FACE_OUTER_BOUND('',#1373,.T.);
#1015=FACE_OUTER_BOUND('',#1374,.T.);
#1016=FACE_OUTER_BOUND('',#1375,.T.);
#1017=FACE_OUTER_BOUND('',#1376,.T.);
#1018=FACE_OUTER_BOUND('',#1377,.T.);
#1019=FACE_OUTER_BOUND('',#1378,.T.);
#1020=FACE_OUTER_BOUND('',#1379,.T.);
#1021=FACE_OUTER_BOUND('',#1380,.T.);
#1022=FACE_OUTER_BOUND('',#1381,.T.);
#1023=FACE_OUTER_BOUND('',#1382,.T.);
#1024=FACE_OUTER_BOUND('',#1383,.T.);
#1336=EDGE_LOOP('',(#4627,#4628,#4629,#4630,#4631,#4632,#4633,#4634,#4635,
#4636,#4637,#4638,#4639,#4640,#4641,#4642,#4643,#4644,#4645,#4646,#4647,
#4648,#4649,#4650,#4651,#4652,#4653,#4654,#4655,#4656,#4657,#4658,#4659,
#4660,#4661,#4662,#4663,#4664,#4665,#4666,#4667,#4668,#4669,#4670));
#1337=EDGE_LOOP('',(#4671));
#1338=EDGE_LOOP('',(#4672,#4673,#4674,#4675));
#1339=EDGE_LOOP('',(#4676,#4677,#4678,#4679));
#1340=EDGE_LOOP('',(#4680,#4681,#4682,#4683));
#1341=EDGE_LOOP('',(#4684,#4685,#4686,#4687));
#1342=EDGE_LOOP('',(#4688,#4689,#4690,#4691));
#1343=EDGE_LOOP('',(#4692,#4693,#4694,#4695));
#1344=EDGE_LOOP('',(#4696,#4697,#4698,#4699));
#1345=EDGE_LOOP('',(#4700,#4701,#4702,#4703));
#1346=EDGE_LOOP('',(#4704,#4705,#4706,#4707));
#1347=EDGE_LOOP('',(#4708,#4709,#4710,#4711));
#1348=EDGE_LOOP('',(#4712,#4713,#4714,#4715));
#1349=EDGE_LOOP('',(#4716,#4717,#4718,#4719));
#1350=EDGE_LOOP('',(#4720,#4721,#4722,#4723));
#1351=EDGE_LOOP('',(#4724,#4725,#4726,#4727));
#1352=EDGE_LOOP('',(#4728,#4729,#4730,#4731));
#1353=EDGE_LOOP('',(#4732,#4733,#4734,#4735));
#1354=EDGE_LOOP('',(#4736,#4737,#4738,#4739));
#1355=EDGE_LOOP('',(#4740,#4741,#4742,#4743));
#1356=EDGE_LOOP('',(#4744,#4745,#4746,#4747));
#1357=EDGE_LOOP('',(#4748,#4749,#4750,#4751));
#1358=EDGE_LOOP('',(#4752,#4753,#4754,#4755));
#1359=EDGE_LOOP('',(#4756,#4757,#4758,#4759));
#1360=EDGE_LOOP('',(#4760,#4761,#4762,#4763));
#1361=EDGE_LOOP('',(#4764,#4765,#4766,#4767));
#1362=EDGE_LOOP('',(#4768,#4769,#4770,#4771));
#1363=EDGE_LOOP('',(#4772,#4773,#4774,#4775));
#1364=EDGE_LOOP('',(#4776,#4777,#4778,#4779));
#1365=EDGE_LOOP('',(#4780,#4781,#4782,#4783));
#1366=EDGE_LOOP('',(#4784,#4785,#4786,#4787));
#1367=EDGE_LOOP('',(#4788,#4789,#4790,#4791));
#1368=EDGE_LOOP('',(#4792,#4793,#4794,#4795));
#1369=EDGE_LOOP('',(#4796,#4797,#4798,#4799));
#1370=EDGE_LOOP('',(#4800,#4801,#4802,#4803));
#1371=EDGE_LOOP('',(#4804,#4805,#4806,#4807));
#1372=EDGE_LOOP('',(#4808,#4809,#4810,#4811));
#1373=EDGE_LOOP('',(#4812,#4813,#4814,#4815));
#1374=EDGE_LOOP('',(#4816,#4817,#4818,#4819));
#1375=EDGE_LOOP('',(#4820,#4821,#4822,#4823));
#1376=EDGE_LOOP('',(#4824,#4825,#4826,#4827));
#1377=EDGE_LOOP('',(#4828,#4829,#4830,#4831));
#1378=EDGE_LOOP('',(#4832,#4833,#4834,#4835));
#1379=EDGE_LOOP('',(#4836,#4837,#4838,#4839));
#1380=EDGE_LOOP('',(#4840,#4841,#4842,#4843));
#1381=EDGE_LOOP('',(#4844,#4845,#4846,#4847));
#1382=EDGE_LOOP('',(#4848,#4849,#4850,#4851));
#1383=EDGE_LOOP('',(#4852,#4853,#4854,#4855,#4856,#4857,#4858,#4859,#4860,
#4861,#4862,#4863,#4864,#4865,#4866,#4867,#4868,#4869,#4870,#4871,#4872,
#4873,#4874,#4875,#4876,#4877,#4878,#4879,#4880,#4881,#4882,#4883,#4884,
#4885,#4886,#4887,#4888,#4889,#4890,#4891,#4892,#4893,#4894,#4895));
#1384=EDGE_LOOP('',(#4896));
#1764=LINE('',#9209,#2308);
#1765=LINE('',#9211,#2309);
#1766=LINE('',#9213,#2310);
#1767=LINE('',#9215,#2311);
#1768=LINE('',#9217,#2312);
#1769=LINE('',#9219,#2313);
#1770=LINE('',#9221,#2314);
#1771=LINE('',#9223,#2315);
#1772=LINE('',#9225,#2316);
#1773=LINE('',#9227,#2317);
#1774=LINE('',#9229,#2318);
#1775=LINE('',#9231,#2319);
#1776=LINE('',#9233,#2320);
#1777=LINE('',#9235,#2321);
#1778=LINE('',#9237,#2322);
#1779=LINE('',#9239,#2323);
#1780=LINE('',#9241,#2324);
#1781=LINE('',#9243,#2325);
#1782=LINE('',#9245,#2326);
#1783=LINE('',#9247,#2327);
#1784=LINE('',#9249,#2328);
#1785=LINE('',#9251,#2329);
#1786=LINE('',#9253,#2330);
#1787=LINE('',#9255,#2331);
#1788=LINE('',#9257,#2332);
#1789=LINE('',#9259,#2333);
#1790=LINE('',#9261,#2334);
#1791=LINE('',#9263,#2335);
#1792=LINE('',#9265,#2336);
#1793=LINE('',#9267,#2337);
#1794=LINE('',#9269,#2338);
#1795=LINE('',#9271,#2339);
#1796=LINE('',#9273,#2340);
#1797=LINE('',#9275,#2341);
#1798=LINE('',#9277,#2342);
#1799=LINE('',#9279,#2343);
#1800=LINE('',#9281,#2344);
#1801=LINE('',#9283,#2345);
#1802=LINE('',#9285,#2346);
#1803=LINE('',#9287,#2347);
#1804=LINE('',#9289,#2348);
#1805=LINE('',#9291,#2349);
#1806=LINE('',#9293,#2350);
#1807=LINE('',#9294,#2351);
#1808=LINE('',#9299,#2352);
#1809=LINE('',#9301,#2353);
#1810=LINE('',#9302,#2354);
#1811=LINE('',#9305,#2355);
#1812=LINE('',#9306,#2356);
#1813=LINE('',#9309,#2357);
#1814=LINE('',#9310,#2358);
#1815=LINE('',#9313,#2359);
#1816=LINE('',#9314,#2360);
#1817=LINE('',#9317,#2361);
#1818=LINE('',#9318,#2362);
#1819=LINE('',#9321,#2363);
#1820=LINE('',#9322,#2364);
#1821=LINE('',#9325,#2365);
#1822=LINE('',#9326,#2366);
#1823=LINE('',#9329,#2367);
#1824=LINE('',#9330,#2368);
#1825=LINE('',#9333,#2369);
#1826=LINE('',#9334,#2370);
#1827=LINE('',#9337,#2371);
#1828=LINE('',#9338,#2372);
#1829=LINE('',#9341,#2373);
#1830=LINE('',#9342,#2374);
#1831=LINE('',#9345,#2375);
#1832=LINE('',#9346,#2376);
#1833=LINE('',#9349,#2377);
#1834=LINE('',#9350,#2378);
#1835=LINE('',#9353,#2379);
#1836=LINE('',#9354,#2380);
#1837=LINE('',#9357,#2381);
#1838=LINE('',#9358,#2382);
#1839=LINE('',#9361,#2383);
#1840=LINE('',#9362,#2384);
#1841=LINE('',#9365,#2385);
#1842=LINE('',#9366,#2386);
#1843=LINE('',#9369,#2387);
#1844=LINE('',#9370,#2388);
#1845=LINE('',#9373,#2389);
#1846=LINE('',#9374,#2390);
#1847=LINE('',#9377,#2391);
#1848=LINE('',#9378,#2392);
#1849=LINE('',#9381,#2393);
#1850=LINE('',#9382,#2394);
#1851=LINE('',#9385,#2395);
#1852=LINE('',#9386,#2396);
#1853=LINE('',#9389,#2397);
#1854=LINE('',#9391,#2398);
#1855=LINE('',#9392,#2399);
#1856=LINE('',#9395,#2400);
#1857=LINE('',#9396,#2401);
#1858=LINE('',#9399,#2402);
#1859=LINE('',#9400,#2403);
#1860=LINE('',#9403,#2404);
#1861=LINE('',#9404,#2405);
#1862=LINE('',#9407,#2406);
#1863=LINE('',#9408,#2407);
#1864=LINE('',#9411,#2408);
#1865=LINE('',#9412,#2409);
#1866=LINE('',#9415,#2410);
#1867=LINE('',#9416,#2411);
#1868=LINE('',#9419,#2412);
#1869=LINE('',#9420,#2413);
#1870=LINE('',#9423,#2414);
#1871=LINE('',#9424,#2415);
#1872=LINE('',#9427,#2416);
#1873=LINE('',#9428,#2417);
#1874=LINE('',#9431,#2418);
#1875=LINE('',#9432,#2419);
#1876=LINE('',#9435,#2420);
#1877=LINE('',#9436,#2421);
#1878=LINE('',#9439,#2422);
#1879=LINE('',#9440,#2423);
#1880=LINE('',#9443,#2424);
#1881=LINE('',#9444,#2425);
#1882=LINE('',#9447,#2426);
#1883=LINE('',#9448,#2427);
#1884=LINE('',#9451,#2428);
#1885=LINE('',#9452,#2429);
#1886=LINE('',#9455,#2430);
#1887=LINE('',#9456,#2431);
#1888=LINE('',#9459,#2432);
#1889=LINE('',#9460,#2433);
#1890=LINE('',#9464,#2434);
#1891=LINE('',#9467,#2435);
#1892=LINE('',#9468,#2436);
#1893=LINE('',#9471,#2437);
#1894=LINE('',#9472,#2438);
#1895=LINE('',#9474,#2439);
#1896=LINE('',#9476,#2440);
#2308=VECTOR('',#7207,1.);
#2309=VECTOR('',#7208,1.);
#2310=VECTOR('',#7209,1.);
#2311=VECTOR('',#7210,1.);
#2312=VECTOR('',#7211,1.);
#2313=VECTOR('',#7212,1.);
#2314=VECTOR('',#7213,1.);
#2315=VECTOR('',#7214,1.);
#2316=VECTOR('',#7215,1.);
#2317=VECTOR('',#7216,1.);
#2318=VECTOR('',#7217,1.);
#2319=VECTOR('',#7218,1.);
#2320=VECTOR('',#7219,1.);
#2321=VECTOR('',#7220,1.);
#2322=VECTOR('',#7221,1.);
#2323=VECTOR('',#7222,1.);
#2324=VECTOR('',#7223,1.);
#2325=VECTOR('',#7224,1.);
#2326=VECTOR('',#7225,1.);
#2327=VECTOR('',#7226,1.);
#2328=VECTOR('',#7227,1.);
#2329=VECTOR('',#7228,1.);
#2330=VECTOR('',#7229,1.);
#2331=VECTOR('',#7230,1.);
#2332=VECTOR('',#7231,1.);
#2333=VECTOR('',#7232,1.);
#2334=VECTOR('',#7233,1.);
#2335=VECTOR('',#7234,1.);
#2336=VECTOR('',#7235,1.);
#2337=VECTOR('',#7236,1.);
#2338=VECTOR('',#7237,1.);
#2339=VECTOR('',#7238,1.);
#2340=VECTOR('',#7239,1.);
#2341=VECTOR('',#7240,1.);
#2342=VECTOR('',#7241,1.);
#2343=VECTOR('',#7242,1.);
#2344=VECTOR('',#7243,1.);
#2345=VECTOR('',#7244,1.);
#2346=VECTOR('',#7245,1.);
#2347=VECTOR('',#7246,1.);
#2348=VECTOR('',#7247,1.);
#2349=VECTOR('',#7248,1.);
#2350=VECTOR('',#7249,1.);
#2351=VECTOR('',#7250,1.);
#2352=VECTOR('',#7255,1.);
#2353=VECTOR('',#7256,1.);
#2354=VECTOR('',#7257,1.);
#2355=VECTOR('',#7260,1.);
#2356=VECTOR('',#7261,1.);
#2357=VECTOR('',#7264,1.);
#2358=VECTOR('',#7265,1.);
#2359=VECTOR('',#7268,1.);
#2360=VECTOR('',#7269,1.);
#2361=VECTOR('',#7272,1.);
#2362=VECTOR('',#7273,1.);
#2363=VECTOR('',#7276,1.);
#2364=VECTOR('',#7277,1.);
#2365=VECTOR('',#7280,1.);
#2366=VECTOR('',#7281,1.);
#2367=VECTOR('',#7284,1.);
#2368=VECTOR('',#7285,1.);
#2369=VECTOR('',#7288,1.);
#2370=VECTOR('',#7289,1.);
#2371=VECTOR('',#7292,1.);
#2372=VECTOR('',#7293,1.);
#2373=VECTOR('',#7296,1.);
#2374=VECTOR('',#7297,1.);
#2375=VECTOR('',#7300,1.);
#2376=VECTOR('',#7301,1.);
#2377=VECTOR('',#7304,1.);
#2378=VECTOR('',#7305,1.);
#2379=VECTOR('',#7308,1.);
#2380=VECTOR('',#7309,1.);
#2381=VECTOR('',#7312,1.);
#2382=VECTOR('',#7313,1.);
#2383=VECTOR('',#7316,1.);
#2384=VECTOR('',#7317,1.);
#2385=VECTOR('',#7320,1.);
#2386=VECTOR('',#7321,1.);
#2387=VECTOR('',#7324,1.);
#2388=VECTOR('',#7325,1.);
#2389=VECTOR('',#7328,1.);
#2390=VECTOR('',#7329,1.);
#2391=VECTOR('',#7332,1.);
#2392=VECTOR('',#7333,1.);
#2393=VECTOR('',#7336,1.);
#2394=VECTOR('',#7337,1.);
#2395=VECTOR('',#7340,1.);
#2396=VECTOR('',#7341,1.);
#2397=VECTOR('',#7344,1.);
#2398=VECTOR('',#7345,1.);
#2399=VECTOR('',#7346,1.);
#2400=VECTOR('',#7349,1.);
#2401=VECTOR('',#7350,1.);
#2402=VECTOR('',#7353,1.);
#2403=VECTOR('',#7354,1.);
#2404=VECTOR('',#7357,1.);
#2405=VECTOR('',#7358,1.);
#2406=VECTOR('',#7361,1.);
#2407=VECTOR('',#7362,1.);
#2408=VECTOR('',#7365,1.);
#2409=VECTOR('',#7366,1.);
#2410=VECTOR('',#7369,1.);
#2411=VECTOR('',#7370,1.);
#2412=VECTOR('',#7373,1.);
#2413=VECTOR('',#7374,1.);
#2414=VECTOR('',#7377,1.);
#2415=VECTOR('',#7378,1.);
#2416=VECTOR('',#7381,1.);
#2417=VECTOR('',#7382,1.);
#2418=VECTOR('',#7385,1.);
#2419=VECTOR('',#7386,1.);
#2420=VECTOR('',#7389,1.);
#2421=VECTOR('',#7390,1.);
#2422=VECTOR('',#7393,1.);
#2423=VECTOR('',#7394,1.);
#2424=VECTOR('',#7397,1.);
#2425=VECTOR('',#7398,1.);
#2426=VECTOR('',#7401,1.);
#2427=VECTOR('',#7402,1.);
#2428=VECTOR('',#7405,1.);
#2429=VECTOR('',#7406,1.);
#2430=VECTOR('',#7409,1.);
#2431=VECTOR('',#7410,1.);
#2432=VECTOR('',#7413,1.);
#2433=VECTOR('',#7414,1.);
#2434=VECTOR('',#7419,0.21);
#2435=VECTOR('',#7422,1.);
#2436=VECTOR('',#7423,1.);
#2437=VECTOR('',#7426,1.);
#2438=VECTOR('',#7427,1.);
#2439=VECTOR('',#7430,1.);
#2440=VECTOR('',#7433,1.);
#2657=CIRCLE('',#6134,0.21);
#2658=CIRCLE('',#6176,0.21);
#2961=VERTEX_POINT('',#9207);
#2962=VERTEX_POINT('',#9208);
#2963=VERTEX_POINT('',#9210);
#2964=VERTEX_POINT('',#9212);
#2965=VERTEX_POINT('',#9214);
#2966=VERTEX_POINT('',#9216);
#2967=VERTEX_POINT('',#9218);
#2968=VERTEX_POINT('',#9220);
#2969=VERTEX_POINT('',#9222);
#2970=VERTEX_POINT('',#9224);
#2971=VERTEX_POINT('',#9226);
#2972=VERTEX_POINT('',#9228);
#2973=VERTEX_POINT('',#9230);
#2974=VERTEX_POINT('',#9232);
#2975=VERTEX_POINT('',#9234);
#2976=VERTEX_POINT('',#9236);
#2977=VERTEX_POINT('',#9238);
#2978=VERTEX_POINT('',#9240);
#2979=VERTEX_POINT('',#9242);
#2980=VERTEX_POINT('',#9244);
#2981=VERTEX_POINT('',#9246);
#2982=VERTEX_POINT('',#9248);
#2983=VERTEX_POINT('',#9250);
#2984=VERTEX_POINT('',#9252);
#2985=VERTEX_POINT('',#9254);
#2986=VERTEX_POINT('',#9256);
#2987=VERTEX_POINT('',#9258);
#2988=VERTEX_POINT('',#9260);
#2989=VERTEX_POINT('',#9262);
#2990=VERTEX_POINT('',#9264);
#2991=VERTEX_POINT('',#9266);
#2992=VERTEX_POINT('',#9268);
#2993=VERTEX_POINT('',#9270);
#2994=VERTEX_POINT('',#9272);
#2995=VERTEX_POINT('',#9274);
#2996=VERTEX_POINT('',#9276);
#2997=VERTEX_POINT('',#9278);
#2998=VERTEX_POINT('',#9280);
#2999=VERTEX_POINT('',#9282);
#3000=VERTEX_POINT('',#9284);
#3001=VERTEX_POINT('',#9286);
#3002=VERTEX_POINT('',#9288);
#3003=VERTEX_POINT('',#9290);
#3004=VERTEX_POINT('',#9292);
#3005=VERTEX_POINT('',#9295);
#3006=VERTEX_POINT('',#9298);
#3007=VERTEX_POINT('',#9300);
#3008=VERTEX_POINT('',#9304);
#3009=VERTEX_POINT('',#9308);
#3010=VERTEX_POINT('',#9312);
#3011=VERTEX_POINT('',#9316);
#3012=VERTEX_POINT('',#9320);
#3013=VERTEX_POINT('',#9324);
#3014=VERTEX_POINT('',#9328);
#3015=VERTEX_POINT('',#9332);
#3016=VERTEX_POINT('',#9336);
#3017=VERTEX_POINT('',#9340);
#3018=VERTEX_POINT('',#9344);
#3019=VERTEX_POINT('',#9348);
#3020=VERTEX_POINT('',#9352);
#3021=VERTEX_POINT('',#9356);
#3022=VERTEX_POINT('',#9360);
#3023=VERTEX_POINT('',#9364);
#3024=VERTEX_POINT('',#9368);
#3025=VERTEX_POINT('',#9372);
#3026=VERTEX_POINT('',#9376);
#3027=VERTEX_POINT('',#9380);
#3028=VERTEX_POINT('',#9384);
#3029=VERTEX_POINT('',#9388);
#3030=VERTEX_POINT('',#9390);
#3031=VERTEX_POINT('',#9394);
#3032=VERTEX_POINT('',#9398);
#3033=VERTEX_POINT('',#9402);
#3034=VERTEX_POINT('',#9406);
#3035=VERTEX_POINT('',#9410);
#3036=VERTEX_POINT('',#9414);
#3037=VERTEX_POINT('',#9418);
#3038=VERTEX_POINT('',#9422);
#3039=VERTEX_POINT('',#9426);
#3040=VERTEX_POINT('',#9430);
#3041=VERTEX_POINT('',#9434);
#3042=VERTEX_POINT('',#9438);
#3043=VERTEX_POINT('',#9442);
#3044=VERTEX_POINT('',#9446);
#3045=VERTEX_POINT('',#9450);
#3046=VERTEX_POINT('',#9454);
#3047=VERTEX_POINT('',#9458);
#3048=VERTEX_POINT('',#9462);
#3049=VERTEX_POINT('',#9466);
#3050=VERTEX_POINT('',#9470);
#3548=EDGE_CURVE('',#2961,#2962,#1764,.T.);
#3549=EDGE_CURVE('',#2963,#2961,#1765,.T.);
#3550=EDGE_CURVE('',#2964,#2963,#1766,.T.);
#3551=EDGE_CURVE('',#2965,#2964,#1767,.T.);
#3552=EDGE_CURVE('',#2966,#2965,#1768,.T.);
#3553=EDGE_CURVE('',#2967,#2966,#1769,.T.);
#3554=EDGE_CURVE('',#2968,#2967,#1770,.T.);
#3555=EDGE_CURVE('',#2969,#2968,#1771,.T.);
#3556=EDGE_CURVE('',#2970,#2969,#1772,.T.);
#3557=EDGE_CURVE('',#2971,#2970,#1773,.T.);
#3558=EDGE_CURVE('',#2972,#2971,#1774,.T.);
#3559=EDGE_CURVE('',#2973,#2972,#1775,.T.);
#3560=EDGE_CURVE('',#2974,#2973,#1776,.T.);
#3561=EDGE_CURVE('',#2975,#2974,#1777,.T.);
#3562=EDGE_CURVE('',#2976,#2975,#1778,.T.);
#3563=EDGE_CURVE('',#2977,#2976,#1779,.T.);
#3564=EDGE_CURVE('',#2978,#2977,#1780,.T.);
#3565=EDGE_CURVE('',#2979,#2978,#1781,.T.);
#3566=EDGE_CURVE('',#2980,#2979,#1782,.T.);
#3567=EDGE_CURVE('',#2981,#2980,#1783,.T.);
#3568=EDGE_CURVE('',#2982,#2981,#1784,.T.);
#3569=EDGE_CURVE('',#2983,#2982,#1785,.T.);
#3570=EDGE_CURVE('',#2984,#2983,#1786,.T.);
#3571=EDGE_CURVE('',#2985,#2984,#1787,.T.);
#3572=EDGE_CURVE('',#2986,#2985,#1788,.T.);
#3573=EDGE_CURVE('',#2987,#2986,#1789,.T.);
#3574=EDGE_CURVE('',#2988,#2987,#1790,.T.);
#3575=EDGE_CURVE('',#2989,#2988,#1791,.T.);
#3576=EDGE_CURVE('',#2990,#2989,#1792,.T.);
#3577=EDGE_CURVE('',#2991,#2990,#1793,.T.);
#3578=EDGE_CURVE('',#2992,#2991,#1794,.T.);
#3579=EDGE_CURVE('',#2993,#2992,#1795,.T.);
#3580=EDGE_CURVE('',#2994,#2993,#1796,.T.);
#3581=EDGE_CURVE('',#2995,#2994,#1797,.T.);
#3582=EDGE_CURVE('',#2996,#2995,#1798,.T.);
#3583=EDGE_CURVE('',#2997,#2996,#1799,.T.);
#3584=EDGE_CURVE('',#2998,#2997,#1800,.T.);
#3585=EDGE_CURVE('',#2999,#2998,#1801,.T.);
#3586=EDGE_CURVE('',#3000,#2999,#1802,.T.);
#3587=EDGE_CURVE('',#3001,#3000,#1803,.T.);
#3588=EDGE_CURVE('',#3002,#3001,#1804,.T.);
#3589=EDGE_CURVE('',#3003,#3002,#1805,.T.);
#3590=EDGE_CURVE('',#3004,#3003,#1806,.T.);
#3591=EDGE_CURVE('',#2962,#3004,#1807,.T.);
#3592=EDGE_CURVE('',#3005,#3005,#2657,.T.);
#3593=EDGE_CURVE('',#3006,#2983,#1808,.T.);
#3594=EDGE_CURVE('',#3007,#3006,#1809,.T.);
#3595=EDGE_CURVE('',#3007,#2984,#1810,.T.);
#3596=EDGE_CURVE('',#3008,#2982,#1811,.T.);
#3597=EDGE_CURVE('',#3008,#3006,#1812,.T.);
#3598=EDGE_CURVE('',#2981,#3009,#1813,.T.);
#3599=EDGE_CURVE('',#3009,#3008,#1814,.T.);
#3600=EDGE_CURVE('',#3010,#2980,#1815,.T.);
#3601=EDGE_CURVE('',#3009,#3010,#1816,.T.);
#3602=EDGE_CURVE('',#3011,#2979,#1817,.T.);
#3603=EDGE_CURVE('',#3010,#3011,#1818,.T.);
#3604=EDGE_CURVE('',#3012,#2978,#1819,.T.);
#3605=EDGE_CURVE('',#3011,#3012,#1820,.T.);
#3606=EDGE_CURVE('',#3013,#2977,#1821,.T.);
#3607=EDGE_CURVE('',#3012,#3013,#1822,.T.);
#3608=EDGE_CURVE('',#3014,#2976,#1823,.T.);
#3609=EDGE_CURVE('',#3013,#3014,#1824,.T.);
#3610=EDGE_CURVE('',#3015,#2975,#1825,.T.);
#3611=EDGE_CURVE('',#3014,#3015,#1826,.T.);
#3612=EDGE_CURVE('',#3016,#2974,#1827,.T.);
#3613=EDGE_CURVE('',#3015,#3016,#1828,.T.);
#3614=EDGE_CURVE('',#3017,#2973,#1829,.T.);
#3615=EDGE_CURVE('',#3016,#3017,#1830,.T.);
#3616=EDGE_CURVE('',#3018,#2972,#1831,.T.);
#3617=EDGE_CURVE('',#3017,#3018,#1832,.T.);
#3618=EDGE_CURVE('',#3019,#2971,#1833,.T.);
#3619=EDGE_CURVE('',#3019,#3018,#1834,.T.);
#3620=EDGE_CURVE('',#2970,#3020,#1835,.T.);
#3621=EDGE_CURVE('',#3020,#3019,#1836,.T.);
#3622=EDGE_CURVE('',#3021,#2969,#1837,.T.);
#3623=EDGE_CURVE('',#3020,#3021,#1838,.T.);
#3624=EDGE_CURVE('',#3022,#2968,#1839,.T.);
#3625=EDGE_CURVE('',#3021,#3022,#1840,.T.);
#3626=EDGE_CURVE('',#3023,#2967,#1841,.T.);
#3627=EDGE_CURVE('',#3022,#3023,#1842,.T.);
#3628=EDGE_CURVE('',#3024,#2966,#1843,.T.);
#3629=EDGE_CURVE('',#3023,#3024,#1844,.T.);
#3630=EDGE_CURVE('',#3025,#2965,#1845,.T.);
#3631=EDGE_CURVE('',#3024,#3025,#1846,.T.);
#3632=EDGE_CURVE('',#3026,#2964,#1847,.T.);
#3633=EDGE_CURVE('',#3025,#3026,#1848,.T.);
#3634=EDGE_CURVE('',#3027,#2963,#1849,.T.);
#3635=EDGE_CURVE('',#3026,#3027,#1850,.T.);
#3636=EDGE_CURVE('',#3028,#2961,#1851,.T.);
#3637=EDGE_CURVE('',#3027,#3028,#1852,.T.);
#3638=EDGE_CURVE('',#3029,#2994,#1853,.T.);
#3639=EDGE_CURVE('',#3030,#3029,#1854,.T.);
#3640=EDGE_CURVE('',#3030,#2995,#1855,.T.);
#3641=EDGE_CURVE('',#3031,#3030,#1856,.T.);
#3642=EDGE_CURVE('',#3031,#2996,#1857,.T.);
#3643=EDGE_CURVE('',#3032,#3031,#1858,.T.);
#3644=EDGE_CURVE('',#3032,#2997,#1859,.T.);
#3645=EDGE_CURVE('',#3033,#3032,#1860,.T.);
#3646=EDGE_CURVE('',#3033,#2998,#1861,.T.);
#3647=EDGE_CURVE('',#3034,#3033,#1862,.T.);
#3648=EDGE_CURVE('',#3034,#2999,#1863,.T.);
#3649=EDGE_CURVE('',#3035,#3034,#1864,.T.);
#3650=EDGE_CURVE('',#3035,#3000,#1865,.T.);
#3651=EDGE_CURVE('',#3036,#3035,#1866,.T.);
#3652=EDGE_CURVE('',#3036,#3001,#1867,.T.);
#3653=EDGE_CURVE('',#3037,#3036,#1868,.T.);
#3654=EDGE_CURVE('',#3037,#3002,#1869,.T.);
#3655=EDGE_CURVE('',#3038,#3037,#1870,.T.);
#3656=EDGE_CURVE('',#3003,#3038,#1871,.T.);
#3657=EDGE_CURVE('',#3039,#3007,#1872,.T.);
#3658=EDGE_CURVE('',#3039,#2985,#1873,.T.);
#3659=EDGE_CURVE('',#3040,#3039,#1874,.T.);
#3660=EDGE_CURVE('',#3040,#2986,#1875,.T.);
#3661=EDGE_CURVE('',#3041,#3040,#1876,.T.);
#3662=EDGE_CURVE('',#3041,#2987,#1877,.T.);
#3663=EDGE_CURVE('',#3042,#3041,#1878,.T.);
#3664=EDGE_CURVE('',#3042,#2988,#1879,.T.);
#3665=EDGE_CURVE('',#3043,#3042,#1880,.T.);
#3666=EDGE_CURVE('',#3043,#2989,#1881,.T.);
#3667=EDGE_CURVE('',#3044,#3043,#1882,.T.);
#3668=EDGE_CURVE('',#3044,#2990,#1883,.T.);
#3669=EDGE_CURVE('',#3045,#3044,#1884,.T.);
#3670=EDGE_CURVE('',#3045,#2991,#1885,.T.);
#3671=EDGE_CURVE('',#3046,#3045,#1886,.T.);
#3672=EDGE_CURVE('',#2992,#3046,#1887,.T.);
#3673=EDGE_CURVE('',#3047,#2962,#1888,.T.);
#3674=EDGE_CURVE('',#3028,#3047,#1889,.T.);
#3675=EDGE_CURVE('',#3048,#3048,#2658,.T.);
#3676=EDGE_CURVE('',#3048,#3005,#1890,.T.);
#3677=EDGE_CURVE('',#3038,#3049,#1891,.T.);
#3678=EDGE_CURVE('',#3049,#3004,#1892,.T.);
#3679=EDGE_CURVE('',#3050,#2993,#1893,.T.);
#3680=EDGE_CURVE('',#3050,#3029,#1894,.T.);
#3681=EDGE_CURVE('',#3046,#3050,#1895,.T.);
#3682=EDGE_CURVE('',#3049,#3047,#1896,.T.);
#4627=ORIENTED_EDGE('',*,*,#3548,.F.);
#4628=ORIENTED_EDGE('',*,*,#3549,.F.);
#4629=ORIENTED_EDGE('',*,*,#3550,.F.);
#4630=ORIENTED_EDGE('',*,*,#3551,.F.);
#4631=ORIENTED_EDGE('',*,*,#3552,.F.);
#4632=ORIENTED_EDGE('',*,*,#3553,.F.);
#4633=ORIENTED_EDGE('',*,*,#3554,.F.);
#4634=ORIENTED_EDGE('',*,*,#3555,.F.);
#4635=ORIENTED_EDGE('',*,*,#3556,.F.);
#4636=ORIENTED_EDGE('',*,*,#3557,.F.);
#4637=ORIENTED_EDGE('',*,*,#3558,.F.);
#4638=ORIENTED_EDGE('',*,*,#3559,.F.);
#4639=ORIENTED_EDGE('',*,*,#3560,.F.);
#4640=ORIENTED_EDGE('',*,*,#3561,.F.);
#4641=ORIENTED_EDGE('',*,*,#3562,.F.);
#4642=ORIENTED_EDGE('',*,*,#3563,.F.);
#4643=ORIENTED_EDGE('',*,*,#3564,.F.);
#4644=ORIENTED_EDGE('',*,*,#3565,.F.);
#4645=ORIENTED_EDGE('',*,*,#3566,.F.);
#4646=ORIENTED_EDGE('',*,*,#3567,.F.);
#4647=ORIENTED_EDGE('',*,*,#3568,.F.);
#4648=ORIENTED_EDGE('',*,*,#3569,.F.);
#4649=ORIENTED_EDGE('',*,*,#3570,.F.);
#4650=ORIENTED_EDGE('',*,*,#3571,.F.);
#4651=ORIENTED_EDGE('',*,*,#3572,.F.);
#4652=ORIENTED_EDGE('',*,*,#3573,.F.);
#4653=ORIENTED_EDGE('',*,*,#3574,.F.);
#4654=ORIENTED_EDGE('',*,*,#3575,.F.);
#4655=ORIENTED_EDGE('',*,*,#3576,.F.);
#4656=ORIENTED_EDGE('',*,*,#3577,.F.);
#4657=ORIENTED_EDGE('',*,*,#3578,.F.);
#4658=ORIENTED_EDGE('',*,*,#3579,.F.);
#4659=ORIENTED_EDGE('',*,*,#3580,.F.);
#4660=ORIENTED_EDGE('',*,*,#3581,.F.);
#4661=ORIENTED_EDGE('',*,*,#3582,.F.);
#4662=ORIENTED_EDGE('',*,*,#3583,.F.);
#4663=ORIENTED_EDGE('',*,*,#3584,.F.);
#4664=ORIENTED_EDGE('',*,*,#3585,.F.);
#4665=ORIENTED_EDGE('',*,*,#3586,.F.);
#4666=ORIENTED_EDGE('',*,*,#3587,.F.);
#4667=ORIENTED_EDGE('',*,*,#3588,.F.);
#4668=ORIENTED_EDGE('',*,*,#3589,.F.);
#4669=ORIENTED_EDGE('',*,*,#3590,.F.);
#4670=ORIENTED_EDGE('',*,*,#3591,.F.);
#4671=ORIENTED_EDGE('',*,*,#3592,.F.);
#4672=ORIENTED_EDGE('',*,*,#3570,.T.);
#4673=ORIENTED_EDGE('',*,*,#3593,.F.);
#4674=ORIENTED_EDGE('',*,*,#3594,.F.);
#4675=ORIENTED_EDGE('',*,*,#3595,.T.);
#4676=ORIENTED_EDGE('',*,*,#3569,.T.);
#4677=ORIENTED_EDGE('',*,*,#3596,.F.);
#4678=ORIENTED_EDGE('',*,*,#3597,.T.);
#4679=ORIENTED_EDGE('',*,*,#3593,.T.);
#4680=ORIENTED_EDGE('',*,*,#3568,.T.);
#4681=ORIENTED_EDGE('',*,*,#3598,.T.);
#4682=ORIENTED_EDGE('',*,*,#3599,.T.);
#4683=ORIENTED_EDGE('',*,*,#3596,.T.);
#4684=ORIENTED_EDGE('',*,*,#3567,.T.);
#4685=ORIENTED_EDGE('',*,*,#3600,.F.);
#4686=ORIENTED_EDGE('',*,*,#3601,.F.);
#4687=ORIENTED_EDGE('',*,*,#3598,.F.);
#4688=ORIENTED_EDGE('',*,*,#3566,.T.);
#4689=ORIENTED_EDGE('',*,*,#3602,.F.);
#4690=ORIENTED_EDGE('',*,*,#3603,.F.);
#4691=ORIENTED_EDGE('',*,*,#3600,.T.);
#4692=ORIENTED_EDGE('',*,*,#3565,.T.);
#4693=ORIENTED_EDGE('',*,*,#3604,.F.);
#4694=ORIENTED_EDGE('',*,*,#3605,.F.);
#4695=ORIENTED_EDGE('',*,*,#3602,.T.);
#4696=ORIENTED_EDGE('',*,*,#3564,.T.);
#4697=ORIENTED_EDGE('',*,*,#3606,.F.);
#4698=ORIENTED_EDGE('',*,*,#3607,.F.);
#4699=ORIENTED_EDGE('',*,*,#3604,.T.);
#4700=ORIENTED_EDGE('',*,*,#3563,.T.);
#4701=ORIENTED_EDGE('',*,*,#3608,.F.);
#4702=ORIENTED_EDGE('',*,*,#3609,.F.);
#4703=ORIENTED_EDGE('',*,*,#3606,.T.);
#4704=ORIENTED_EDGE('',*,*,#3562,.T.);
#4705=ORIENTED_EDGE('',*,*,#3610,.F.);
#4706=ORIENTED_EDGE('',*,*,#3611,.F.);
#4707=ORIENTED_EDGE('',*,*,#3608,.T.);
#4708=ORIENTED_EDGE('',*,*,#3561,.T.);
#4709=ORIENTED_EDGE('',*,*,#3612,.F.);
#4710=ORIENTED_EDGE('',*,*,#3613,.F.);
#4711=ORIENTED_EDGE('',*,*,#3610,.T.);
#4712=ORIENTED_EDGE('',*,*,#3560,.T.);
#4713=ORIENTED_EDGE('',*,*,#3614,.F.);
#4714=ORIENTED_EDGE('',*,*,#3615,.F.);
#4715=ORIENTED_EDGE('',*,*,#3612,.T.);
#4716=ORIENTED_EDGE('',*,*,#3559,.T.);
#4717=ORIENTED_EDGE('',*,*,#3616,.F.);
#4718=ORIENTED_EDGE('',*,*,#3617,.F.);
#4719=ORIENTED_EDGE('',*,*,#3614,.T.);
#4720=ORIENTED_EDGE('',*,*,#3558,.T.);
#4721=ORIENTED_EDGE('',*,*,#3618,.F.);
#4722=ORIENTED_EDGE('',*,*,#3619,.T.);
#4723=ORIENTED_EDGE('',*,*,#3616,.T.);
#4724=ORIENTED_EDGE('',*,*,#3557,.T.);
#4725=ORIENTED_EDGE('',*,*,#3620,.T.);
#4726=ORIENTED_EDGE('',*,*,#3621,.T.);
#4727=ORIENTED_EDGE('',*,*,#3618,.T.);
#4728=ORIENTED_EDGE('',*,*,#3556,.T.);
#4729=ORIENTED_EDGE('',*,*,#3622,.F.);
#4730=ORIENTED_EDGE('',*,*,#3623,.F.);
#4731=ORIENTED_EDGE('',*,*,#3620,.F.);
#4732=ORIENTED_EDGE('',*,*,#3555,.T.);
#4733=ORIENTED_EDGE('',*,*,#3624,.F.);
#4734=ORIENTED_EDGE('',*,*,#3625,.F.);
#4735=ORIENTED_EDGE('',*,*,#3622,.T.);
#4736=ORIENTED_EDGE('',*,*,#3554,.T.);
#4737=ORIENTED_EDGE('',*,*,#3626,.F.);
#4738=ORIENTED_EDGE('',*,*,#3627,.F.);
#4739=ORIENTED_EDGE('',*,*,#3624,.T.);
#4740=ORIENTED_EDGE('',*,*,#3553,.T.);
#4741=ORIENTED_EDGE('',*,*,#3628,.F.);
#4742=ORIENTED_EDGE('',*,*,#3629,.F.);
#4743=ORIENTED_EDGE('',*,*,#3626,.T.);
#4744=ORIENTED_EDGE('',*,*,#3552,.T.);
#4745=ORIENTED_EDGE('',*,*,#3630,.F.);
#4746=ORIENTED_EDGE('',*,*,#3631,.F.);
#4747=ORIENTED_EDGE('',*,*,#3628,.T.);
#4748=ORIENTED_EDGE('',*,*,#3551,.T.);
#4749=ORIENTED_EDGE('',*,*,#3632,.F.);
#4750=ORIENTED_EDGE('',*,*,#3633,.F.);
#4751=ORIENTED_EDGE('',*,*,#3630,.T.);
#4752=ORIENTED_EDGE('',*,*,#3550,.T.);
#4753=ORIENTED_EDGE('',*,*,#3634,.F.);
#4754=ORIENTED_EDGE('',*,*,#3635,.F.);
#4755=ORIENTED_EDGE('',*,*,#3632,.T.);
#4756=ORIENTED_EDGE('',*,*,#3549,.T.);
#4757=ORIENTED_EDGE('',*,*,#3636,.F.);
#4758=ORIENTED_EDGE('',*,*,#3637,.F.);
#4759=ORIENTED_EDGE('',*,*,#3634,.T.);
#4760=ORIENTED_EDGE('',*,*,#3581,.T.);
#4761=ORIENTED_EDGE('',*,*,#3638,.F.);
#4762=ORIENTED_EDGE('',*,*,#3639,.F.);
#4763=ORIENTED_EDGE('',*,*,#3640,.T.);
#4764=ORIENTED_EDGE('',*,*,#3582,.T.);
#4765=ORIENTED_EDGE('',*,*,#3640,.F.);
#4766=ORIENTED_EDGE('',*,*,#3641,.F.);
#4767=ORIENTED_EDGE('',*,*,#3642,.T.);
#4768=ORIENTED_EDGE('',*,*,#3583,.T.);
#4769=ORIENTED_EDGE('',*,*,#3642,.F.);
#4770=ORIENTED_EDGE('',*,*,#3643,.F.);
#4771=ORIENTED_EDGE('',*,*,#3644,.T.);
#4772=ORIENTED_EDGE('',*,*,#3584,.T.);
#4773=ORIENTED_EDGE('',*,*,#3644,.F.);
#4774=ORIENTED_EDGE('',*,*,#3645,.F.);
#4775=ORIENTED_EDGE('',*,*,#3646,.T.);
#4776=ORIENTED_EDGE('',*,*,#3585,.T.);
#4777=ORIENTED_EDGE('',*,*,#3646,.F.);
#4778=ORIENTED_EDGE('',*,*,#3647,.F.);
#4779=ORIENTED_EDGE('',*,*,#3648,.T.);
#4780=ORIENTED_EDGE('',*,*,#3586,.T.);
#4781=ORIENTED_EDGE('',*,*,#3648,.F.);
#4782=ORIENTED_EDGE('',*,*,#3649,.F.);
#4783=ORIENTED_EDGE('',*,*,#3650,.T.);
#4784=ORIENTED_EDGE('',*,*,#3587,.T.);
#4785=ORIENTED_EDGE('',*,*,#3650,.F.);
#4786=ORIENTED_EDGE('',*,*,#3651,.F.);
#4787=ORIENTED_EDGE('',*,*,#3652,.T.);
#4788=ORIENTED_EDGE('',*,*,#3588,.T.);
#4789=ORIENTED_EDGE('',*,*,#3652,.F.);
#4790=ORIENTED_EDGE('',*,*,#3653,.F.);
#4791=ORIENTED_EDGE('',*,*,#3654,.T.);
#4792=ORIENTED_EDGE('',*,*,#3589,.T.);
#4793=ORIENTED_EDGE('',*,*,#3654,.F.);
#4794=ORIENTED_EDGE('',*,*,#3655,.F.);
#4795=ORIENTED_EDGE('',*,*,#3656,.F.);
#4796=ORIENTED_EDGE('',*,*,#3571,.T.);
#4797=ORIENTED_EDGE('',*,*,#3595,.F.);
#4798=ORIENTED_EDGE('',*,*,#3657,.F.);
#4799=ORIENTED_EDGE('',*,*,#3658,.T.);
#4800=ORIENTED_EDGE('',*,*,#3572,.T.);
#4801=ORIENTED_EDGE('',*,*,#3658,.F.);
#4802=ORIENTED_EDGE('',*,*,#3659,.F.);
#4803=ORIENTED_EDGE('',*,*,#3660,.T.);
#4804=ORIENTED_EDGE('',*,*,#3573,.T.);
#4805=ORIENTED_EDGE('',*,*,#3660,.F.);
#4806=ORIENTED_EDGE('',*,*,#3661,.F.);
#4807=ORIENTED_EDGE('',*,*,#3662,.T.);
#4808=ORIENTED_EDGE('',*,*,#3574,.T.);
#4809=ORIENTED_EDGE('',*,*,#3662,.F.);
#4810=ORIENTED_EDGE('',*,*,#3663,.F.);
#4811=ORIENTED_EDGE('',*,*,#3664,.T.);
#4812=ORIENTED_EDGE('',*,*,#3575,.T.);
#4813=ORIENTED_EDGE('',*,*,#3664,.F.);
#4814=ORIENTED_EDGE('',*,*,#3665,.F.);
#4815=ORIENTED_EDGE('',*,*,#3666,.T.);
#4816=ORIENTED_EDGE('',*,*,#3576,.T.);
#4817=ORIENTED_EDGE('',*,*,#3666,.F.);
#4818=ORIENTED_EDGE('',*,*,#3667,.F.);
#4819=ORIENTED_EDGE('',*,*,#3668,.T.);
#4820=ORIENTED_EDGE('',*,*,#3577,.T.);
#4821=ORIENTED_EDGE('',*,*,#3668,.F.);
#4822=ORIENTED_EDGE('',*,*,#3669,.F.);
#4823=ORIENTED_EDGE('',*,*,#3670,.T.);
#4824=ORIENTED_EDGE('',*,*,#3578,.T.);
#4825=ORIENTED_EDGE('',*,*,#3670,.F.);
#4826=ORIENTED_EDGE('',*,*,#3671,.F.);
#4827=ORIENTED_EDGE('',*,*,#3672,.F.);
#4828=ORIENTED_EDGE('',*,*,#3548,.T.);
#4829=ORIENTED_EDGE('',*,*,#3673,.F.);
#4830=ORIENTED_EDGE('',*,*,#3674,.F.);
#4831=ORIENTED_EDGE('',*,*,#3636,.T.);
#4832=ORIENTED_EDGE('',*,*,#3675,.F.);
#4833=ORIENTED_EDGE('',*,*,#3676,.T.);
#4834=ORIENTED_EDGE('',*,*,#3592,.T.);
#4835=ORIENTED_EDGE('',*,*,#3676,.F.);
#4836=ORIENTED_EDGE('',*,*,#3590,.T.);
#4837=ORIENTED_EDGE('',*,*,#3656,.T.);
#4838=ORIENTED_EDGE('',*,*,#3677,.T.);
#4839=ORIENTED_EDGE('',*,*,#3678,.T.);
#4840=ORIENTED_EDGE('',*,*,#3580,.T.);
#4841=ORIENTED_EDGE('',*,*,#3679,.F.);
#4842=ORIENTED_EDGE('',*,*,#3680,.T.);
#4843=ORIENTED_EDGE('',*,*,#3638,.T.);
#4844=ORIENTED_EDGE('',*,*,#3579,.T.);
#4845=ORIENTED_EDGE('',*,*,#3672,.T.);
#4846=ORIENTED_EDGE('',*,*,#3681,.T.);
#4847=ORIENTED_EDGE('',*,*,#3679,.T.);
#4848=ORIENTED_EDGE('',*,*,#3591,.T.);
#4849=ORIENTED_EDGE('',*,*,#3678,.F.);
#4850=ORIENTED_EDGE('',*,*,#3682,.T.);
#4851=ORIENTED_EDGE('',*,*,#3673,.T.);
#4852=ORIENTED_EDGE('',*,*,#3639,.T.);
#4853=ORIENTED_EDGE('',*,*,#3680,.F.);
#4854=ORIENTED_EDGE('',*,*,#3681,.F.);
#4855=ORIENTED_EDGE('',*,*,#3671,.T.);
#4856=ORIENTED_EDGE('',*,*,#3669,.T.);
#4857=ORIENTED_EDGE('',*,*,#3667,.T.);
#4858=ORIENTED_EDGE('',*,*,#3665,.T.);
#4859=ORIENTED_EDGE('',*,*,#3663,.T.);
#4860=ORIENTED_EDGE('',*,*,#3661,.T.);
#4861=ORIENTED_EDGE('',*,*,#3659,.T.);
#4862=ORIENTED_EDGE('',*,*,#3657,.T.);
#4863=ORIENTED_EDGE('',*,*,#3594,.T.);
#4864=ORIENTED_EDGE('',*,*,#3597,.F.);
#4865=ORIENTED_EDGE('',*,*,#3599,.F.);
#4866=ORIENTED_EDGE('',*,*,#3601,.T.);
#4867=ORIENTED_EDGE('',*,*,#3603,.T.);
#4868=ORIENTED_EDGE('',*,*,#3605,.T.);
#4869=ORIENTED_EDGE('',*,*,#3607,.T.);
#4870=ORIENTED_EDGE('',*,*,#3609,.T.);
#4871=ORIENTED_EDGE('',*,*,#3611,.T.);
#4872=ORIENTED_EDGE('',*,*,#3613,.T.);
#4873=ORIENTED_EDGE('',*,*,#3615,.T.);
#4874=ORIENTED_EDGE('',*,*,#3617,.T.);
#4875=ORIENTED_EDGE('',*,*,#3619,.F.);
#4876=ORIENTED_EDGE('',*,*,#3621,.F.);
#4877=ORIENTED_EDGE('',*,*,#3623,.T.);
#4878=ORIENTED_EDGE('',*,*,#3625,.T.);
#4879=ORIENTED_EDGE('',*,*,#3627,.T.);
#4880=ORIENTED_EDGE('',*,*,#3629,.T.);
#4881=ORIENTED_EDGE('',*,*,#3631,.T.);
#4882=ORIENTED_EDGE('',*,*,#3633,.T.);
#4883=ORIENTED_EDGE('',*,*,#3635,.T.);
#4884=ORIENTED_EDGE('',*,*,#3637,.T.);
#4885=ORIENTED_EDGE('',*,*,#3674,.T.);
#4886=ORIENTED_EDGE('',*,*,#3682,.F.);
#4887=ORIENTED_EDGE('',*,*,#3677,.F.);
#4888=ORIENTED_EDGE('',*,*,#3655,.T.);
#4889=ORIENTED_EDGE('',*,*,#3653,.T.);
#4890=ORIENTED_EDGE('',*,*,#3651,.T.);
#4891=ORIENTED_EDGE('',*,*,#3649,.T.);
#4892=ORIENTED_EDGE('',*,*,#3647,.T.);
#4893=ORIENTED_EDGE('',*,*,#3645,.T.);
#4894=ORIENTED_EDGE('',*,*,#3643,.T.);
#4895=ORIENTED_EDGE('',*,*,#3641,.T.);
#4896=ORIENTED_EDGE('',*,*,#3675,.T.);
#5306=CYLINDRICAL_SURFACE('',#6175,0.21);
#5474=ADVANCED_FACE('',(#978,#597),#717,.T.);
#5475=ADVANCED_FACE('',(#979),#718,.F.);
#5476=ADVANCED_FACE('',(#980),#719,.T.);
#5477=ADVANCED_FACE('',(#981),#720,.T.);
#5478=ADVANCED_FACE('',(#982),#721,.F.);
#5479=ADVANCED_FACE('',(#983),#722,.F.);
#5480=ADVANCED_FACE('',(#984),#723,.F.);
#5481=ADVANCED_FACE('',(#985),#724,.F.);
#5482=ADVANCED_FACE('',(#986),#725,.F.);
#5483=ADVANCED_FACE('',(#987),#726,.F.);
#5484=ADVANCED_FACE('',(#988),#727,.F.);
#5485=ADVANCED_FACE('',(#989),#728,.F.);
#5486=ADVANCED_FACE('',(#990),#729,.F.);
#5487=ADVANCED_FACE('',(#991),#730,.T.);
#5488=ADVANCED_FACE('',(#992),#731,.T.);
#5489=ADVANCED_FACE('',(#993),#732,.F.);
#5490=ADVANCED_FACE('',(#994),#733,.F.);
#5491=ADVANCED_FACE('',(#995),#734,.F.);
#5492=ADVANCED_FACE('',(#996),#735,.F.);
#5493=ADVANCED_FACE('',(#997),#736,.F.);
#5494=ADVANCED_FACE('',(#998),#737,.F.);
#5495=ADVANCED_FACE('',(#999),#738,.F.);
#5496=ADVANCED_FACE('',(#1000),#739,.F.);
#5497=ADVANCED_FACE('',(#1001),#740,.F.);
#5498=ADVANCED_FACE('',(#1002),#741,.F.);
#5499=ADVANCED_FACE('',(#1003),#742,.F.);
#5500=ADVANCED_FACE('',(#1004),#743,.F.);
#5501=ADVANCED_FACE('',(#1005),#744,.F.);
#5502=ADVANCED_FACE('',(#1006),#745,.F.);
#5503=ADVANCED_FACE('',(#1007),#746,.F.);
#5504=ADVANCED_FACE('',(#1008),#747,.F.);
#5505=ADVANCED_FACE('',(#1009),#748,.F.);
#5506=ADVANCED_FACE('',(#1010),#749,.F.);
#5507=ADVANCED_FACE('',(#1011),#750,.F.);
#5508=ADVANCED_FACE('',(#1012),#751,.F.);
#5509=ADVANCED_FACE('',(#1013),#752,.F.);
#5510=ADVANCED_FACE('',(#1014),#753,.F.);
#5511=ADVANCED_FACE('',(#1015),#754,.F.);
#5512=ADVANCED_FACE('',(#1016),#755,.F.);
#5513=ADVANCED_FACE('',(#1017),#756,.F.);
#5514=ADVANCED_FACE('',(#1018),#757,.F.);
#5515=ADVANCED_FACE('',(#1019),#5306,.F.);
#5516=ADVANCED_FACE('',(#1020),#758,.T.);
#5517=ADVANCED_FACE('',(#1021),#759,.T.);
#5518=ADVANCED_FACE('',(#1022),#760,.T.);
#5519=ADVANCED_FACE('',(#1023),#761,.T.);
#5520=ADVANCED_FACE('',(#1024,#598),#762,.F.);
#5627=CLOSED_SHELL('',(#5474,#5475,#5476,#5477,#5478,#5479,#5480,#5481,
#5482,#5483,#5484,#5485,#5486,#5487,#5488,#5489,#5490,#5491,#5492,#5493,
#5494,#5495,#5496,#5497,#5498,#5499,#5500,#5501,#5502,#5503,#5504,#5505,
#5506,#5507,#5508,#5509,#5510,#5511,#5512,#5513,#5514,#5515,#5516,#5517,
#5518,#5519,#5520));
#6132=AXIS2_PLACEMENT_3D('',#9205,#7203,#7204);
#6133=AXIS2_PLACEMENT_3D('',#9206,#7205,#7206);
#6134=AXIS2_PLACEMENT_3D('',#9296,#7251,#7252);
#6135=AXIS2_PLACEMENT_3D('',#9297,#7253,#7254);
#6136=AXIS2_PLACEMENT_3D('',#9303,#7258,#7259);
#6137=AXIS2_PLACEMENT_3D('',#9307,#7262,#7263);
#6138=AXIS2_PLACEMENT_3D('',#9311,#7266,#7267);
#6139=AXIS2_PLACEMENT_3D('',#9315,#7270,#7271);
#6140=AXIS2_PLACEMENT_3D('',#9319,#7274,#7275);
#6141=AXIS2_PLACEMENT_3D('',#9323,#7278,#7279);
#6142=AXIS2_PLACEMENT_3D('',#9327,#7282,#7283);
#6143=AXIS2_PLACEMENT_3D('',#9331,#7286,#7287);
#6144=AXIS2_PLACEMENT_3D('',#9335,#7290,#7291);
#6145=AXIS2_PLACEMENT_3D('',#9339,#7294,#7295);
#6146=AXIS2_PLACEMENT_3D('',#9343,#7298,#7299);
#6147=AXIS2_PLACEMENT_3D('',#9347,#7302,#7303);
#6148=AXIS2_PLACEMENT_3D('',#9351,#7306,#7307);
#6149=AXIS2_PLACEMENT_3D('',#9355,#7310,#7311);
#6150=AXIS2_PLACEMENT_3D('',#9359,#7314,#7315);
#6151=AXIS2_PLACEMENT_3D('',#9363,#7318,#7319);
#6152=AXIS2_PLACEMENT_3D('',#9367,#7322,#7323);
#6153=AXIS2_PLACEMENT_3D('',#9371,#7326,#7327);
#6154=AXIS2_PLACEMENT_3D('',#9375,#7330,#7331);
#6155=AXIS2_PLACEMENT_3D('',#9379,#7334,#7335);
#6156=AXIS2_PLACEMENT_3D('',#9383,#7338,#7339);
#6157=AXIS2_PLACEMENT_3D('',#9387,#7342,#7343);
#6158=AXIS2_PLACEMENT_3D('',#9393,#7347,#7348);
#6159=AXIS2_PLACEMENT_3D('',#9397,#7351,#7352);
#6160=AXIS2_PLACEMENT_3D('',#9401,#7355,#7356);
#6161=AXIS2_PLACEMENT_3D('',#9405,#7359,#7360);
#6162=AXIS2_PLACEMENT_3D('',#9409,#7363,#7364);
#6163=AXIS2_PLACEMENT_3D('',#9413,#7367,#7368);
#6164=AXIS2_PLACEMENT_3D('',#9417,#7371,#7372);
#6165=AXIS2_PLACEMENT_3D('',#9421,#7375,#7376);
#6166=AXIS2_PLACEMENT_3D('',#9425,#7379,#7380);
#6167=AXIS2_PLACEMENT_3D('',#9429,#7383,#7384);
#6168=AXIS2_PLACEMENT_3D('',#9433,#7387,#7388);
#6169=AXIS2_PLACEMENT_3D('',#9437,#7391,#7392);
#6170=AXIS2_PLACEMENT_3D('',#9441,#7395,#7396);
#6171=AXIS2_PLACEMENT_3D('',#9445,#7399,#7400);
#6172=AXIS2_PLACEMENT_3D('',#9449,#7403,#7404);
#6173=AXIS2_PLACEMENT_3D('',#9453,#7407,#7408);
#6174=AXIS2_PLACEMENT_3D('',#9457,#7411,#7412);
#6175=AXIS2_PLACEMENT_3D('',#9461,#7415,#7416);
#6176=AXIS2_PLACEMENT_3D('',#9463,#7417,#7418);
#6177=AXIS2_PLACEMENT_3D('',#9465,#7420,#7421);
#6178=AXIS2_PLACEMENT_3D('',#9469,#7424,#7425);
#6179=AXIS2_PLACEMENT_3D('',#9473,#7428,#7429);
#6180=AXIS2_PLACEMENT_3D('',#9475,#7431,#7432);
#6181=AXIS2_PLACEMENT_3D('',#9477,#7434,#7435);
#7203=DIRECTION('axis',(0.,0.,1.));
#7204=DIRECTION('refdir',(1.,0.,0.));
#7205=DIRECTION('center_axis',(1.,0.,0.));
#7206=DIRECTION('ref_axis',(0.,0.,-1.));
#7207=DIRECTION('',(0.,0.,1.));
#7208=DIRECTION('',(0.,-1.,0.));
#7209=DIRECTION('',(0.,0.,1.));
#7210=DIRECTION('',(0.,0.707106781186548,0.707106781186547));
#7211=DIRECTION('',(0.,1.,0.));
#7212=DIRECTION('',(0.,0.707106781186548,-0.707106781186547));
#7213=DIRECTION('',(0.,0.,-1.));
#7214=DIRECTION('',(0.,-1.,0.));
#7215=DIRECTION('',(0.,0.,-1.));
#7216=DIRECTION('',(0.,1.,0.));
#7217=DIRECTION('',(0.,0.,1.));
#7218=DIRECTION('',(0.,-1.,0.));
#7219=DIRECTION('',(0.,0.,-1.));
#7220=DIRECTION('',(0.,-1.,0.));
#7221=DIRECTION('',(0.,-0.707106781186548,0.707106781186548));
#7222=DIRECTION('',(0.,0.,1.));
#7223=DIRECTION('',(0.,0.707106781186547,0.707106781186548));
#7224=DIRECTION('',(0.,1.,-7.40148683083438E-16));
#7225=DIRECTION('',(0.,0.,-1.));
#7226=DIRECTION('',(0.,1.,0.));
#7227=DIRECTION('',(0.,0.,1.));
#7228=DIRECTION('',(0.,-1.,0.));
#7229=DIRECTION('',(0.,-2.41352831440251E-16,-1.));
#7230=DIRECTION('',(0.,1.,0.));
#7231=DIRECTION('',(0.,0.,-1.));
#7232=DIRECTION('',(0.,-0.707106781186548,-0.707106781186547));
#7233=DIRECTION('',(0.,-1.,0.));
#7234=DIRECTION('',(0.,-0.707106781186547,0.707106781186548));
#7235=DIRECTION('',(0.,0.,1.));
#7236=DIRECTION('',(0.,1.,0.));
#7237=DIRECTION('',(0.,2.41352831440251E-16,1.));
#7238=DIRECTION('',(0.,-1.,0.));
#7239=DIRECTION('',(0.,0.,-1.));
#7240=DIRECTION('',(0.,1.,0.));
#7241=DIRECTION('',(0.,8.88178419700125E-16,1.));
#7242=DIRECTION('',(0.,1.,-7.40148683083439E-16));
#7243=DIRECTION('',(0.,0.707106781186548,-0.707106781186547));
#7244=DIRECTION('',(0.,-2.77555756156289E-16,-1.));
#7245=DIRECTION('',(0.,-0.707106781186548,-0.707106781186547));
#7246=DIRECTION('',(0.,-1.,7.40148683083438E-16));
#7247=DIRECTION('',(0.,4.44089209850063E-16,1.));
#7248=DIRECTION('',(0.,-1.,2.41352831440251E-16));
#7249=DIRECTION('',(0.,0.,-1.));
#7250=DIRECTION('',(0.,1.,0.));
#7251=DIRECTION('center_axis',(1.,0.,0.));
#7252=DIRECTION('ref_axis',(0.,0.,-1.));
#7253=DIRECTION('center_axis',(0.,-1.,2.41352831440251E-16));
#7254=DIRECTION('ref_axis',(0.,-2.41352831440251E-16,-1.));
#7255=DIRECTION('',(1.,0.,0.));
#7256=DIRECTION('',(0.,-2.41352831440251E-16,-1.));
#7257=DIRECTION('',(1.,0.,0.));
#7258=DIRECTION('center_axis',(0.,0.,-1.));
#7259=DIRECTION('ref_axis',(0.,1.,0.));
#7260=DIRECTION('',(1.,0.,0.));
#7261=DIRECTION('',(0.,1.,0.));
#7262=DIRECTION('center_axis',(0.,-1.,0.));
#7263=DIRECTION('ref_axis',(0.,0.,-1.));
#7264=DIRECTION('',(-1.,0.,0.));
#7265=DIRECTION('',(0.,0.,-1.));
#7266=DIRECTION('center_axis',(0.,0.,-1.));
#7267=DIRECTION('ref_axis',(0.,1.,0.));
#7268=DIRECTION('',(1.,0.,0.));
#7269=DIRECTION('',(0.,1.,0.));
#7270=DIRECTION('center_axis',(0.,-1.,0.));
#7271=DIRECTION('ref_axis',(0.,0.,-1.));
#7272=DIRECTION('',(1.,0.,0.));
#7273=DIRECTION('',(0.,0.,-1.));
#7274=DIRECTION('center_axis',(0.,-7.40148683083438E-16,-1.));
#7275=DIRECTION('ref_axis',(0.,1.,-7.40148683083438E-16));
#7276=DIRECTION('',(1.,0.,0.));
#7277=DIRECTION('',(0.,1.,-7.40148683083438E-16));
#7278=DIRECTION('center_axis',(0.,0.707106781186548,-0.707106781186547));
#7279=DIRECTION('ref_axis',(0.,0.707106781186547,0.707106781186548));
#7280=DIRECTION('',(1.,0.,0.));
#7281=DIRECTION('',(0.,0.707106781186547,0.707106781186548));
#7282=DIRECTION('center_axis',(0.,1.,0.));
#7283=DIRECTION('ref_axis',(0.,0.,1.));
#7284=DIRECTION('',(1.,0.,0.));
#7285=DIRECTION('',(0.,0.,1.));
#7286=DIRECTION('center_axis',(0.,0.707106781186548,0.707106781186548));
#7287=DIRECTION('ref_axis',(0.,-0.707106781186548,0.707106781186548));
#7288=DIRECTION('',(1.,0.,0.));
#7289=DIRECTION('',(0.,-0.707106781186548,0.707106781186548));
#7290=DIRECTION('center_axis',(0.,0.,1.));
#7291=DIRECTION('ref_axis',(0.,-1.,0.));
#7292=DIRECTION('',(1.,0.,0.));
#7293=DIRECTION('',(0.,-1.,0.));
#7294=DIRECTION('center_axis',(0.,-1.,0.));
#7295=DIRECTION('ref_axis',(0.,0.,-1.));
#7296=DIRECTION('',(1.,0.,0.));
#7297=DIRECTION('',(0.,0.,-1.));
#7298=DIRECTION('center_axis',(0.,0.,1.));
#7299=DIRECTION('ref_axis',(0.,-1.,0.));
#7300=DIRECTION('',(1.,0.,0.));
#7301=DIRECTION('',(0.,-1.,0.));
#7302=DIRECTION('center_axis',(0.,-1.,0.));
#7303=DIRECTION('ref_axis',(0.,0.,-1.));
#7304=DIRECTION('',(1.,0.,0.));
#7305=DIRECTION('',(0.,0.,-1.));
#7306=DIRECTION('center_axis',(0.,0.,1.));
#7307=DIRECTION('ref_axis',(0.,-1.,0.));
#7308=DIRECTION('',(-1.,0.,0.));
#7309=DIRECTION('',(0.,-1.,0.));
#7310=DIRECTION('center_axis',(0.,-1.,0.));
#7311=DIRECTION('ref_axis',(0.,0.,-1.));
#7312=DIRECTION('',(1.,0.,0.));
#7313=DIRECTION('',(0.,0.,-1.));
#7314=DIRECTION('center_axis',(0.,0.,1.));
#7315=DIRECTION('ref_axis',(0.,-1.,0.));
#7316=DIRECTION('',(1.,0.,0.));
#7317=DIRECTION('',(0.,-1.,0.));
#7318=DIRECTION('center_axis',(0.,-1.,0.));
#7319=DIRECTION('ref_axis',(0.,0.,-1.));
#7320=DIRECTION('',(1.,0.,0.));
#7321=DIRECTION('',(0.,0.,-1.));
#7322=DIRECTION('center_axis',(0.,-0.707106781186547,-0.707106781186548));
#7323=DIRECTION('ref_axis',(0.,0.707106781186548,-0.707106781186547));
#7324=DIRECTION('',(1.,0.,0.));
#7325=DIRECTION('',(0.,0.707106781186548,-0.707106781186547));
#7326=DIRECTION('center_axis',(0.,0.,-1.));
#7327=DIRECTION('ref_axis',(0.,1.,0.));
#7328=DIRECTION('',(1.,0.,0.));
#7329=DIRECTION('',(0.,1.,0.));
#7330=DIRECTION('center_axis',(0.,0.707106781186547,-0.707106781186548));
#7331=DIRECTION('ref_axis',(0.,0.707106781186548,0.707106781186547));
#7332=DIRECTION('',(1.,0.,0.));
#7333=DIRECTION('',(0.,0.707106781186548,0.707106781186547));
#7334=DIRECTION('center_axis',(0.,1.,0.));
#7335=DIRECTION('ref_axis',(0.,0.,1.));
#7336=DIRECTION('',(1.,0.,0.));
#7337=DIRECTION('',(0.,0.,1.));
#7338=DIRECTION('center_axis',(0.,0.,1.));
#7339=DIRECTION('ref_axis',(0.,-1.,0.));
#7340=DIRECTION('',(1.,0.,0.));
#7341=DIRECTION('',(0.,-1.,0.));
#7342=DIRECTION('center_axis',(0.,0.,-1.));
#7343=DIRECTION('ref_axis',(0.,1.,0.));
#7344=DIRECTION('',(1.,0.,0.));
#7345=DIRECTION('',(0.,1.,0.));
#7346=DIRECTION('',(1.,0.,0.));
#7347=DIRECTION('center_axis',(0.,1.,-8.88178419700125E-16));
#7348=DIRECTION('ref_axis',(0.,8.88178419700125E-16,1.));
#7349=DIRECTION('',(0.,8.88178419700125E-16,1.));
#7350=DIRECTION('',(1.,0.,0.));
#7351=DIRECTION('center_axis',(0.,-7.40148683083439E-16,-1.));
#7352=DIRECTION('ref_axis',(0.,1.,-7.40148683083439E-16));
#7353=DIRECTION('',(0.,1.,-7.40148683083439E-16));
#7354=DIRECTION('',(1.,0.,0.));
#7355=DIRECTION('center_axis',(0.,-0.707106781186547,-0.707106781186548));
#7356=DIRECTION('ref_axis',(0.,0.707106781186548,-0.707106781186547));
#7357=DIRECTION('',(0.,0.707106781186548,-0.707106781186547));
#7358=DIRECTION('',(1.,0.,0.));
#7359=DIRECTION('center_axis',(0.,-1.,2.77555756156289E-16));
#7360=DIRECTION('ref_axis',(0.,-2.77555756156289E-16,-1.));
#7361=DIRECTION('',(0.,-2.77555756156289E-16,-1.));
#7362=DIRECTION('',(1.,0.,0.));
#7363=DIRECTION('center_axis',(0.,-0.707106781186547,0.707106781186548));
#7364=DIRECTION('ref_axis',(0.,-0.707106781186548,-0.707106781186547));
#7365=DIRECTION('',(0.,-0.707106781186548,-0.707106781186547));
#7366=DIRECTION('',(1.,0.,0.));
#7367=DIRECTION('center_axis',(0.,7.40148683083438E-16,1.));
#7368=DIRECTION('ref_axis',(0.,-1.,7.40148683083438E-16));
#7369=DIRECTION('',(0.,-1.,7.40148683083438E-16));
#7370=DIRECTION('',(1.,0.,0.));
#7371=DIRECTION('center_axis',(0.,1.,-4.44089209850063E-16));
#7372=DIRECTION('ref_axis',(0.,4.44089209850063E-16,1.));
#7373=DIRECTION('',(0.,4.44089209850063E-16,1.));
#7374=DIRECTION('',(1.,0.,0.));
#7375=DIRECTION('center_axis',(0.,2.41352831440251E-16,1.));
#7376=DIRECTION('ref_axis',(0.,-1.,2.41352831440251E-16));
#7377=DIRECTION('',(0.,-1.,2.41352831440251E-16));
#7378=DIRECTION('',(-1.,0.,0.));
#7379=DIRECTION('center_axis',(0.,0.,-1.));
#7380=DIRECTION('ref_axis',(0.,1.,0.));
#7381=DIRECTION('',(0.,1.,0.));
#7382=DIRECTION('',(1.,0.,0.));
#7383=DIRECTION('center_axis',(0.,-1.,0.));
#7384=DIRECTION('ref_axis',(0.,0.,-1.));
#7385=DIRECTION('',(0.,0.,-1.));
#7386=DIRECTION('',(1.,0.,0.));
#7387=DIRECTION('center_axis',(0.,-0.707106781186547,0.707106781186548));
#7388=DIRECTION('ref_axis',(0.,-0.707106781186548,-0.707106781186547));
#7389=DIRECTION('',(0.,-0.707106781186548,-0.707106781186547));
#7390=DIRECTION('',(1.,0.,0.));
#7391=DIRECTION('center_axis',(0.,0.,1.));
#7392=DIRECTION('ref_axis',(0.,-1.,0.));
#7393=DIRECTION('',(0.,-1.,0.));
#7394=DIRECTION('',(1.,0.,0.));
#7395=DIRECTION('center_axis',(0.,0.707106781186548,0.707106781186547));
#7396=DIRECTION('ref_axis',(0.,-0.707106781186547,0.707106781186548));
#7397=DIRECTION('',(0.,-0.707106781186547,0.707106781186548));
#7398=DIRECTION('',(1.,0.,0.));
#7399=DIRECTION('center_axis',(0.,1.,0.));
#7400=DIRECTION('ref_axis',(0.,0.,1.));
#7401=DIRECTION('',(0.,0.,1.));
#7402=DIRECTION('',(1.,0.,0.));
#7403=DIRECTION('center_axis',(0.,0.,-1.));
#7404=DIRECTION('ref_axis',(0.,1.,0.));
#7405=DIRECTION('',(0.,1.,0.));
#7406=DIRECTION('',(1.,0.,0.));
#7407=DIRECTION('center_axis',(0.,1.,-2.41352831440251E-16));
#7408=DIRECTION('ref_axis',(0.,2.41352831440251E-16,1.));
#7409=DIRECTION('',(0.,2.41352831440251E-16,1.));
#7410=DIRECTION('',(-1.,0.,0.));
#7411=DIRECTION('center_axis',(0.,1.,0.));
#7412=DIRECTION('ref_axis',(0.,0.,1.));
#7413=DIRECTION('',(1.,0.,0.));
#7414=DIRECTION('',(0.,0.,1.));
#7415=DIRECTION('center_axis',(1.,0.,0.));
#7416=DIRECTION('ref_axis',(0.,0.,-1.));
#7417=DIRECTION('center_axis',(1.,0.,0.));
#7418=DIRECTION('ref_axis',(0.,0.,-1.));
#7419=DIRECTION('',(1.,0.,0.));
#7420=DIRECTION('center_axis',(0.,1.,0.));
#7421=DIRECTION('ref_axis',(0.,0.,1.));
#7422=DIRECTION('',(0.,0.,1.));
#7423=DIRECTION('',(1.,0.,0.));
#7424=DIRECTION('center_axis',(0.,1.,0.));
#7425=DIRECTION('ref_axis',(0.,0.,1.));
#7426=DIRECTION('',(1.,0.,0.));
#7427=DIRECTION('',(0.,0.,1.));
#7428=DIRECTION('center_axis',(0.,0.,-1.));
#7429=DIRECTION('ref_axis',(0.,1.,0.));
#7430=DIRECTION('',(0.,1.,0.));
#7431=DIRECTION('center_axis',(0.,0.,1.));
#7432=DIRECTION('ref_axis',(0.,-1.,0.));
#7433=DIRECTION('',(0.,-1.,0.));
#7434=DIRECTION('center_axis',(1.,0.,0.));
#7435=DIRECTION('ref_axis',(0.,0.,-1.));
#9205=CARTESIAN_POINT('',(0.,0.,0.));
#9206=CARTESIAN_POINT('Origin',(36.,0.,0.));
#9207=CARTESIAN_POINT('',(36.,0.3,0.82));
#9208=CARTESIAN_POINT('',(36.,0.3,1.));
#9209=CARTESIAN_POINT('',(36.,0.3,0.41));
#9210=CARTESIAN_POINT('',(36.,0.55,0.82));
#9211=CARTESIAN_POINT('',(36.,0.275,0.82));
#9212=CARTESIAN_POINT('',(36.,0.55,0.67));
#9213=CARTESIAN_POINT('',(36.,0.55,0.335));
#9214=CARTESIAN_POINT('',(36.,0.3,0.42));
#9215=CARTESIAN_POINT('',(36.,0.12,0.24));
#9216=CARTESIAN_POINT('',(36.,-0.3,0.42));
#9217=CARTESIAN_POINT('',(36.,-0.15,0.42));
#9218=CARTESIAN_POINT('',(36.,-0.55,0.67));
#9219=CARTESIAN_POINT('',(36.,-0.245,0.365));
#9220=CARTESIAN_POINT('',(36.,-0.55,0.82));
#9221=CARTESIAN_POINT('',(36.,-0.55,0.41));
#9222=CARTESIAN_POINT('',(36.,-0.3,0.82));
#9223=CARTESIAN_POINT('',(36.,-0.15,0.82));
#9224=CARTESIAN_POINT('',(36.,-0.3,1.));
#9225=CARTESIAN_POINT('',(36.,-0.3,0.525));
#9226=CARTESIAN_POINT('',(36.,-1.,1.));
#9227=CARTESIAN_POINT('',(36.,0.5,1.));
#9228=CARTESIAN_POINT('',(36.,-1.,0.3));
#9229=CARTESIAN_POINT('',(36.,-1.,0.5));
#9230=CARTESIAN_POINT('',(36.,-0.82,0.3));
#9231=CARTESIAN_POINT('',(36.,-0.41,0.3));
#9232=CARTESIAN_POINT('',(36.,-0.82,0.55));
#9233=CARTESIAN_POINT('',(36.,-0.82,0.275));
#9234=CARTESIAN_POINT('',(36.,-0.67,0.55));
#9235=CARTESIAN_POINT('',(36.,-0.335,0.55));
#9236=CARTESIAN_POINT('',(36.,-0.42,0.3));
#9237=CARTESIAN_POINT('',(36.,-0.24,0.12));
#9238=CARTESIAN_POINT('',(36.,-0.42,-0.3));
#9239=CARTESIAN_POINT('',(36.,-0.42,-0.15));
#9240=CARTESIAN_POINT('',(36.,-0.67,-0.55));
#9241=CARTESIAN_POINT('',(36.,-0.365,-0.245));
#9242=CARTESIAN_POINT('',(36.,-0.82,-0.55));
#9243=CARTESIAN_POINT('',(36.,-0.41,-0.55));
#9244=CARTESIAN_POINT('',(36.,-0.82,-0.3));
#9245=CARTESIAN_POINT('',(36.,-0.82,-0.15));
#9246=CARTESIAN_POINT('',(36.,-1.,-0.3));
#9247=CARTESIAN_POINT('',(36.,-0.525,-0.3));
#9248=CARTESIAN_POINT('',(36.,-1.,-1.));
#9249=CARTESIAN_POINT('',(36.,-1.,0.5));
#9250=CARTESIAN_POINT('',(36.,-0.3,-1.));
#9251=CARTESIAN_POINT('',(36.,-0.5,-1.));
#9252=CARTESIAN_POINT('',(36.,-0.3,-0.82));
#9253=CARTESIAN_POINT('',(36.,-0.3,-0.41));
#9254=CARTESIAN_POINT('',(36.,-0.55,-0.82));
#9255=CARTESIAN_POINT('',(36.,-0.275,-0.82));
#9256=CARTESIAN_POINT('',(36.,-0.55,-0.67));
#9257=CARTESIAN_POINT('',(36.,-0.55,-0.335));
#9258=CARTESIAN_POINT('',(36.,-0.3,-0.42));
#9259=CARTESIAN_POINT('',(36.,-0.12,-0.24));
#9260=CARTESIAN_POINT('',(36.,0.3,-0.42));
#9261=CARTESIAN_POINT('',(36.,0.15,-0.42));
#9262=CARTESIAN_POINT('',(36.,0.55,-0.67));
#9263=CARTESIAN_POINT('',(36.,0.245,-0.365));
#9264=CARTESIAN_POINT('',(36.,0.55,-0.82));
#9265=CARTESIAN_POINT('',(36.,0.55,-0.41));
#9266=CARTESIAN_POINT('',(36.,0.3,-0.82));
#9267=CARTESIAN_POINT('',(36.,0.15,-0.82));
#9268=CARTESIAN_POINT('',(36.,0.3,-1.));
#9269=CARTESIAN_POINT('',(36.,0.3,-0.525));
#9270=CARTESIAN_POINT('',(36.,1.,-1.));
#9271=CARTESIAN_POINT('',(36.,-0.5,-1.));
#9272=CARTESIAN_POINT('',(36.,1.,-0.3));
#9273=CARTESIAN_POINT('',(36.,1.,-0.5));
#9274=CARTESIAN_POINT('',(36.,0.82,-0.3));
#9275=CARTESIAN_POINT('',(36.,0.41,-0.3));
#9276=CARTESIAN_POINT('',(36.,0.82,-0.55));
#9277=CARTESIAN_POINT('',(36.,0.82,-0.275));
#9278=CARTESIAN_POINT('',(36.,0.67,-0.55));
#9279=CARTESIAN_POINT('',(36.,0.335,-0.55));
#9280=CARTESIAN_POINT('',(36.,0.42,-0.3));
#9281=CARTESIAN_POINT('',(36.,0.24,-0.12));
#9282=CARTESIAN_POINT('',(36.,0.42,0.3));
#9283=CARTESIAN_POINT('',(36.,0.42,0.15));
#9284=CARTESIAN_POINT('',(36.,0.67,0.55));
#9285=CARTESIAN_POINT('',(36.,0.365,0.245));
#9286=CARTESIAN_POINT('',(36.,0.82,0.55));
#9287=CARTESIAN_POINT('',(36.,0.41,0.55));
#9288=CARTESIAN_POINT('',(36.,0.82,0.3));
#9289=CARTESIAN_POINT('',(36.,0.82,0.15));
#9290=CARTESIAN_POINT('',(36.,1.,0.3));
#9291=CARTESIAN_POINT('',(36.,0.525,0.3));
#9292=CARTESIAN_POINT('',(36.,1.,1.));
#9293=CARTESIAN_POINT('',(36.,1.,-0.5));
#9294=CARTESIAN_POINT('',(36.,0.5,1.));
#9295=CARTESIAN_POINT('',(36.,-2.57175827820944E-17,0.21));
#9296=CARTESIAN_POINT('Origin',(36.,0.,0.));
#9297=CARTESIAN_POINT('Origin',(-0.1,-0.3,-0.82));
#9298=CARTESIAN_POINT('',(0.,-0.3,-1.));
#9299=CARTESIAN_POINT('',(-0.05,-0.3,-1.));
#9300=CARTESIAN_POINT('',(0.,-0.3,-0.82));
#9301=CARTESIAN_POINT('',(0.,-0.3,-0.41));
#9302=CARTESIAN_POINT('',(-0.1,-0.3,-0.82));
#9303=CARTESIAN_POINT('Origin',(0.,-1.,-1.));
#9304=CARTESIAN_POINT('',(0.,-1.,-1.));
#9305=CARTESIAN_POINT('',(0.,-1.,-1.));
#9306=CARTESIAN_POINT('',(0.,-1.,-1.));
#9307=CARTESIAN_POINT('Origin',(0.,-1.,1.));
#9308=CARTESIAN_POINT('',(0.,-1.,-0.3));
#9309=CARTESIAN_POINT('',(-0.05,-1.,-0.3));
#9310=CARTESIAN_POINT('',(0.,-1.,1.));
#9311=CARTESIAN_POINT('Origin',(-0.1,-1.05,-0.3));
#9312=CARTESIAN_POINT('',(0.,-0.82,-0.3));
#9313=CARTESIAN_POINT('',(-0.1,-0.82,-0.3));
#9314=CARTESIAN_POINT('',(0.,-0.525,-0.3));
#9315=CARTESIAN_POINT('Origin',(-0.1,-0.82,-0.3));
#9316=CARTESIAN_POINT('',(0.,-0.82,-0.55));
#9317=CARTESIAN_POINT('',(-0.1,-0.82,-0.55));
#9318=CARTESIAN_POINT('',(0.,-0.82,-0.15));
#9319=CARTESIAN_POINT('Origin',(-0.1,-0.82,-0.55));
#9320=CARTESIAN_POINT('',(0.,-0.67,-0.55));
#9321=CARTESIAN_POINT('',(-0.1,-0.67,-0.55));
#9322=CARTESIAN_POINT('',(0.,-0.41,-0.55));
#9323=CARTESIAN_POINT('Origin',(-0.1,-0.67,-0.55));
#9324=CARTESIAN_POINT('',(0.,-0.42,-0.3));
#9325=CARTESIAN_POINT('',(-0.1,-0.42,-0.3));
#9326=CARTESIAN_POINT('',(0.,-0.365,-0.245));
#9327=CARTESIAN_POINT('Origin',(-0.1,-0.42,-0.3));
#9328=CARTESIAN_POINT('',(0.,-0.42,0.3));
#9329=CARTESIAN_POINT('',(-0.1,-0.42,0.3));
#9330=CARTESIAN_POINT('',(0.,-0.42,-0.15));
#9331=CARTESIAN_POINT('Origin',(-0.1,-0.42,0.3));
#9332=CARTESIAN_POINT('',(0.,-0.67,0.55));
#9333=CARTESIAN_POINT('',(-0.1,-0.67,0.55));
#9334=CARTESIAN_POINT('',(-6.93889390390723E-18,-0.24,0.12));
#9335=CARTESIAN_POINT('Origin',(-0.1,-0.67,0.55));
#9336=CARTESIAN_POINT('',(0.,-0.82,0.55));
#9337=CARTESIAN_POINT('',(-0.1,-0.82,0.55));
#9338=CARTESIAN_POINT('',(0.,-0.335,0.55));
#9339=CARTESIAN_POINT('Origin',(-0.1,-0.82,0.55));
#9340=CARTESIAN_POINT('',(0.,-0.82,0.3));
#9341=CARTESIAN_POINT('',(-0.1,-0.82,0.3));
#9342=CARTESIAN_POINT('',(0.,-0.82,0.275));
#9343=CARTESIAN_POINT('Origin',(-0.1,-0.82,0.3));
#9344=CARTESIAN_POINT('',(0.,-1.,0.3));
#9345=CARTESIAN_POINT('',(-0.05,-1.,0.3));
#9346=CARTESIAN_POINT('',(0.,-0.41,0.3));
#9347=CARTESIAN_POINT('Origin',(0.,-1.,1.));
#9348=CARTESIAN_POINT('',(0.,-1.,1.));
#9349=CARTESIAN_POINT('',(0.,-1.,1.));
#9350=CARTESIAN_POINT('',(0.,-1.,1.));
#9351=CARTESIAN_POINT('Origin',(0.,1.,1.));
#9352=CARTESIAN_POINT('',(0.,-0.3,1.));
#9353=CARTESIAN_POINT('',(-0.05,-0.3,1.));
#9354=CARTESIAN_POINT('',(0.,1.,1.));
#9355=CARTESIAN_POINT('Origin',(-0.1,-0.3,1.05));
#9356=CARTESIAN_POINT('',(0.,-0.3,0.82));
#9357=CARTESIAN_POINT('',(-0.1,-0.3,0.82));
#9358=CARTESIAN_POINT('',(0.,-0.3,0.525));
#9359=CARTESIAN_POINT('Origin',(-0.1,-0.3,0.82));
#9360=CARTESIAN_POINT('',(0.,-0.55,0.82));
#9361=CARTESIAN_POINT('',(-0.1,-0.55,0.82));
#9362=CARTESIAN_POINT('',(0.,-0.15,0.82));
#9363=CARTESIAN_POINT('Origin',(-0.1,-0.55,0.82));
#9364=CARTESIAN_POINT('',(0.,-0.55,0.67));
#9365=CARTESIAN_POINT('',(-0.1,-0.55,0.67));
#9366=CARTESIAN_POINT('',(0.,-0.55,0.41));
#9367=CARTESIAN_POINT('Origin',(-0.1,-0.55,0.67));
#9368=CARTESIAN_POINT('',(0.,-0.3,0.42));
#9369=CARTESIAN_POINT('',(-0.1,-0.3,0.42));
#9370=CARTESIAN_POINT('',(6.93889390390723E-18,-0.245,0.365));
#9371=CARTESIAN_POINT('Origin',(-0.1,-0.3,0.42));
#9372=CARTESIAN_POINT('',(0.,0.3,0.42));
#9373=CARTESIAN_POINT('',(-0.1,0.3,0.42));
#9374=CARTESIAN_POINT('',(0.,-0.15,0.42));
#9375=CARTESIAN_POINT('Origin',(-0.1,0.3,0.42));
#9376=CARTESIAN_POINT('',(0.,0.55,0.67));
#9377=CARTESIAN_POINT('',(-0.1,0.55,0.67));
#9378=CARTESIAN_POINT('',(6.93889390390723E-18,0.12,0.24));
#9379=CARTESIAN_POINT('Origin',(-0.1,0.55,0.67));
#9380=CARTESIAN_POINT('',(0.,0.55,0.82));
#9381=CARTESIAN_POINT('',(-0.1,0.55,0.82));
#9382=CARTESIAN_POINT('',(0.,0.55,0.335));
#9383=CARTESIAN_POINT('Origin',(-0.1,0.55,0.82));
#9384=CARTESIAN_POINT('',(0.,0.3,0.82));
#9385=CARTESIAN_POINT('',(-0.1,0.3,0.82));
#9386=CARTESIAN_POINT('',(0.,0.275,0.82));
#9387=CARTESIAN_POINT('Origin',(-0.1,0.82,-0.3));
#9388=CARTESIAN_POINT('',(0.,1.,-0.3));
#9389=CARTESIAN_POINT('',(-0.05,1.,-0.3));
#9390=CARTESIAN_POINT('',(0.,0.82,-0.3));
#9391=CARTESIAN_POINT('',(0.,0.41,-0.3));
#9392=CARTESIAN_POINT('',(-0.1,0.82,-0.3));
#9393=CARTESIAN_POINT('Origin',(-0.1,0.82,-0.55));
#9394=CARTESIAN_POINT('',(0.,0.82,-0.55));
#9395=CARTESIAN_POINT('',(0.,0.82,-0.275));
#9396=CARTESIAN_POINT('',(-0.1,0.82,-0.55));
#9397=CARTESIAN_POINT('Origin',(-0.1,0.67,-0.55));
#9398=CARTESIAN_POINT('',(0.,0.67,-0.55));
#9399=CARTESIAN_POINT('',(0.,0.335,-0.55));
#9400=CARTESIAN_POINT('',(-0.1,0.67,-0.55));
#9401=CARTESIAN_POINT('Origin',(-0.1,0.42,-0.3));
#9402=CARTESIAN_POINT('',(0.,0.42,-0.3));
#9403=CARTESIAN_POINT('',(0.,0.24,-0.12));
#9404=CARTESIAN_POINT('',(-0.1,0.42,-0.3));
#9405=CARTESIAN_POINT('Origin',(-0.1,0.42,0.3));
#9406=CARTESIAN_POINT('',(0.,0.42,0.3));
#9407=CARTESIAN_POINT('',(0.,0.42,0.15));
#9408=CARTESIAN_POINT('',(-0.1,0.42,0.3));
#9409=CARTESIAN_POINT('Origin',(-0.1,0.67,0.55));
#9410=CARTESIAN_POINT('',(0.,0.67,0.55));
#9411=CARTESIAN_POINT('',(6.93889390390723E-18,0.365,0.245));
#9412=CARTESIAN_POINT('',(-0.1,0.67,0.55));
#9413=CARTESIAN_POINT('Origin',(-0.1,0.82,0.55));
#9414=CARTESIAN_POINT('',(0.,0.82,0.55));
#9415=CARTESIAN_POINT('',(0.,0.41,0.55));
#9416=CARTESIAN_POINT('',(-0.1,0.82,0.55));
#9417=CARTESIAN_POINT('Origin',(-0.1,0.82,0.3));
#9418=CARTESIAN_POINT('',(0.,0.82,0.3));
#9419=CARTESIAN_POINT('',(0.,0.82,0.15));
#9420=CARTESIAN_POINT('',(-0.1,0.82,0.3));
#9421=CARTESIAN_POINT('Origin',(-0.1,1.05,0.3));
#9422=CARTESIAN_POINT('',(0.,1.,0.3));
#9423=CARTESIAN_POINT('',(0.,0.525,0.3));
#9424=CARTESIAN_POINT('',(-0.05,1.,0.3));
#9425=CARTESIAN_POINT('Origin',(-0.1,-0.55,-0.82));
#9426=CARTESIAN_POINT('',(0.,-0.55,-0.82));
#9427=CARTESIAN_POINT('',(0.,-0.275,-0.82));
#9428=CARTESIAN_POINT('',(-0.1,-0.55,-0.82));
#9429=CARTESIAN_POINT('Origin',(-0.1,-0.55,-0.67));
#9430=CARTESIAN_POINT('',(0.,-0.55,-0.67));
#9431=CARTESIAN_POINT('',(0.,-0.55,-0.335));
#9432=CARTESIAN_POINT('',(-0.1,-0.55,-0.67));
#9433=CARTESIAN_POINT('Origin',(-0.1,-0.3,-0.42));
#9434=CARTESIAN_POINT('',(0.,-0.3,-0.42));
#9435=CARTESIAN_POINT('',(0.,-0.12,-0.24));
#9436=CARTESIAN_POINT('',(-0.1,-0.3,-0.42));
#9437=CARTESIAN_POINT('Origin',(-0.1,0.3,-0.42));
#9438=CARTESIAN_POINT('',(0.,0.3,-0.42));
#9439=CARTESIAN_POINT('',(0.,0.15,-0.42));
#9440=CARTESIAN_POINT('',(-0.1,0.3,-0.42));
#9441=CARTESIAN_POINT('Origin',(-0.1,0.55,-0.67));
#9442=CARTESIAN_POINT('',(0.,0.55,-0.67));
#9443=CARTESIAN_POINT('',(0.,0.245,-0.365));
#9444=CARTESIAN_POINT('',(-0.1,0.55,-0.67));
#9445=CARTESIAN_POINT('Origin',(-0.1,0.55,-0.82));
#9446=CARTESIAN_POINT('',(0.,0.55,-0.82));
#9447=CARTESIAN_POINT('',(0.,0.55,-0.41));
#9448=CARTESIAN_POINT('',(-0.1,0.55,-0.82));
#9449=CARTESIAN_POINT('Origin',(-0.1,0.3,-0.82));
#9450=CARTESIAN_POINT('',(0.,0.3,-0.82));
#9451=CARTESIAN_POINT('',(0.,0.15,-0.82));
#9452=CARTESIAN_POINT('',(-0.1,0.3,-0.82));
#9453=CARTESIAN_POINT('Origin',(-0.1,0.3,-1.05));
#9454=CARTESIAN_POINT('',(0.,0.3,-1.));
#9455=CARTESIAN_POINT('',(0.,0.3,-0.525));
#9456=CARTESIAN_POINT('',(-0.05,0.3,-1.));
#9457=CARTESIAN_POINT('Origin',(-0.1,0.3,0.82));
#9458=CARTESIAN_POINT('',(0.,0.3,1.));
#9459=CARTESIAN_POINT('',(-0.05,0.3,1.));
#9460=CARTESIAN_POINT('',(0.,0.3,0.41));
#9461=CARTESIAN_POINT('Origin',(-0.1,0.,0.));
#9462=CARTESIAN_POINT('',(0.,-2.57175827820944E-17,0.21));
#9463=CARTESIAN_POINT('Origin',(0.,0.,0.));
#9464=CARTESIAN_POINT('',(-0.1,-2.57175827820944E-17,0.21));
#9465=CARTESIAN_POINT('Origin',(0.,1.,-1.));
#9466=CARTESIAN_POINT('',(0.,1.,1.));
#9467=CARTESIAN_POINT('',(0.,1.,-1.));
#9468=CARTESIAN_POINT('',(0.,1.,1.));
#9469=CARTESIAN_POINT('Origin',(0.,1.,-1.));
#9470=CARTESIAN_POINT('',(0.,1.,-1.));
#9471=CARTESIAN_POINT('',(0.,1.,-1.));
#9472=CARTESIAN_POINT('',(0.,1.,-1.));
#9473=CARTESIAN_POINT('Origin',(0.,-1.,-1.));
#9474=CARTESIAN_POINT('',(0.,-1.,-1.));
#9475=CARTESIAN_POINT('Origin',(0.,1.,1.));
#9476=CARTESIAN_POINT('',(0.,1.,1.));
#9477=CARTESIAN_POINT('Origin',(0.,0.,0.));
#9987=UNCERTAINTY_MEASURE_WITH_UNIT(LENGTH_MEASURE(0.001),#10020,
'DISTANCE_ACCURACY_VALUE',
'Maximum model space distance between geometric entities at asserted c
onnectivities');
#9995=UNCERTAINTY_MEASURE_WITH_UNIT(LENGTH_MEASURE(0.001),#10020,
'DISTANCE_ACCURACY_VALUE',
'Maximum model space distance between geometric entities at asserted c
onnectivities');
#10011=(
GEOMETRIC_REPRESENTATION_CONTEXT(3)
GLOBAL_UNCERTAINTY_ASSIGNED_CONTEXT((#9987))
GLOBAL_UNIT_ASSIGNED_CONTEXT((#10020,#10022,#10023))
REPRESENTATION_CONTEXT('','3D')
);
#10019=(
GEOMETRIC_REPRESENTATION_CONTEXT(3)
GLOBAL_UNCERTAINTY_ASSIGNED_CONTEXT((#9995))
GLOBAL_UNIT_ASSIGNED_CONTEXT((#10020,#10022,#10023))
REPRESENTATION_CONTEXT('','3D')
);
#10020=(
LENGTH_UNIT()
NAMED_UNIT(*)
SI_UNIT(.CENTI.,.METRE.)
);
#10022=(
NAMED_UNIT(*)
PLANE_ANGLE_UNIT()
SI_UNIT($,.RADIAN.)
);
#10023=(
NAMED_UNIT(*)
SI_UNIT($,.STERADIAN.)
SOLID_ANGLE_UNIT()
);
#10039=SHAPE_DEFINITION_REPRESENTATION(#10062,#10182);
#10062=PRODUCT_DEFINITION_SHAPE('',$,#10206);
#10182=SHAPE_REPRESENTATION('',(#6132),#10011);
#10190=PRODUCT_DEFINITION_CONTEXT('part definition',#10261,'design');
#10206=PRODUCT_DEFINITION('360 mm cross member',
'360 mm cross member',#10229,#10190);
#10229=PRODUCT_DEFINITION_FORMATION('',$,#10278);
#10261=APPLICATION_CONTEXT(
'Core Data for Automotive Mechanical Design Process');
#10262=PRODUCT_CONTEXT('part definition',#10261,'mechanical');
#10278=PRODUCT('360 mm cross member','360 mm cross member',
'360 mm cross member',(#10262));
#10356=COLOUR_RGB('Off White',0.89,0.88,0.83);
#10357=FILL_AREA_STYLE_COLOUR('',#10356);
#10358=FILL_AREA_STYLE('',(#10357));
#10359=SURFACE_STYLE_FILL_AREA(#10358);
#10360=SURFACE_SIDE_STYLE('',(#10359));
#10361=SURFACE_STYLE_USAGE(.BOTH.,#10360);
#10362=PRESENTATION_STYLE_ASSIGNMENT((#10361));
ENDSEC;
END-ISO-10303-21;
